ISO-10303-21;
HEADER;
/* Generated by software containing ST-Developer
 * from STEP Tools, Inc. (www.steptools.com) 
 */

FILE_DESCRIPTION(
/* description */ (''),
/* implementation_level */ '2;1');

FILE_NAME(
/* name */ 'Configuration 1.step',
/* time_stamp */ '2026-10-06T10:18:54-07:00',
/* author */ (''),
/* organization */ (''),
/* preprocessor_version */ 'ST-DEVELOPER v20.2',
/* originating_system */ 'Autodesk Translation Framework v15.15.0.0',
/* authorisation */ '');

FILE_SCHEMA (('AUTOMOTIVE_DESIGN { 1 0 10303 214 3 1 1 }'));
ENDSEC;

DATA;
#10=MECHANICAL_DESIGN_GEOMETRIC_PRESENTATION_REPRESENTATION('',(#81),#8445);
#63=SHAPE_REPRESENTATION_RELATIONSHIP('SRR','None',#8484,#72);
#72=ADVANCED_BREP_SHAPE_REPRESENTATION('',(#90),#8436);
#81=STYLED_ITEM('',(#8537),#90);
#90=MANIFOLD_SOLID_BREP('Body1',#4002);
#99=CONICAL_SURFACE('',#4273,1.5,0.523598775598299);
#100=CONICAL_SURFACE('',#4276,1.5,0.523598775598299);
#102=SPHERICAL_SURFACE('',#4234,3.);
#103=SPHERICAL_SURFACE('',#4236,3.);
#104=CYLINDRICAL_SURFACE('',#4148,3.);
#105=CYLINDRICAL_SURFACE('',#4152,3.);
#106=CYLINDRICAL_SURFACE('',#4156,3.);
#107=CYLINDRICAL_SURFACE('',#4162,3.);
#108=CYLINDRICAL_SURFACE('',#4177,3.);
#109=CYLINDRICAL_SURFACE('',#4178,28.);
#110=CYLINDRICAL_SURFACE('',#4187,28.);
#111=CYLINDRICAL_SURFACE('',#4202,3.);
#112=CYLINDRICAL_SURFACE('',#4203,3.);
#113=CYLINDRICAL_SURFACE('',#4210,3.);
#114=CYLINDRICAL_SURFACE('',#4216,3.);
#115=CYLINDRICAL_SURFACE('',#4230,3.);
#116=CYLINDRICAL_SURFACE('',#4232,3.);
#117=CYLINDRICAL_SURFACE('',#4238,28.);
#118=CYLINDRICAL_SURFACE('',#4240,3.);
#119=CYLINDRICAL_SURFACE('',#4243,5.99999999999999);
#120=CYLINDRICAL_SURFACE('',#4245,17.5);
#121=CYLINDRICAL_SURFACE('',#4247,5.99999999999999);
#122=CYLINDRICAL_SURFACE('',#4250,3.);
#123=CYLINDRICAL_SURFACE('',#4254,9.5);
#124=CYLINDRICAL_SURFACE('',#4258,3.);
#125=CYLINDRICAL_SURFACE('',#4260,3.);
#126=CYLINDRICAL_SURFACE('',#4263,3.);
#127=CYLINDRICAL_SURFACE('',#4264,4.);
#128=CYLINDRICAL_SURFACE('',#4266,28.);
#129=CYLINDRICAL_SURFACE('',#4268,4.);
#130=CYLINDRICAL_SURFACE('',#4269,3.99999999999999);
#131=CYLINDRICAL_SURFACE('',#4271,3.99999999999999);
#132=CYLINDRICAL_SURFACE('',#4275,3.);
#133=CYLINDRICAL_SURFACE('',#4278,3.);
#134=CYLINDRICAL_SURFACE('',#4281,35.);
#169=ELLIPSE('',#4142,6.70820393249937,3.);
#170=ELLIPSE('',#4143,6.70820393249937,3.);
#171=ELLIPSE('',#4171,6.70820393249937,3.);
#172=ELLIPSE('',#4172,6.70820393249937,3.);
#173=ELLIPSE('',#4180,6.70820393249938,3.);
#174=ELLIPSE('',#4181,6.70820393249937,3.);
#175=ELLIPSE('',#4191,3.00051436158052,3.);
#176=ELLIPSE('',#4193,6.00025719732504,6.);
#177=ELLIPSE('',#4200,6.70820393249937,3.);
#178=ELLIPSE('',#4201,6.70820393249938,3.);
#179=ELLIPSE('',#4204,3.00051436158052,3.);
#180=ELLIPSE('',#4208,6.00025719732504,6.);
#181=ELLIPSE('',#4218,6.0005786784788,5.99999999999999);
#182=ELLIPSE('',#4220,9.00038579598755,8.99999999999999);
#183=ELLIPSE('',#4222,14.5006215602022,14.5);
#184=ELLIPSE('',#4223,17.5005150104847,17.5);
#185=ELLIPSE('',#4224,9.00038579598755,8.99999999999999);
#186=ELLIPSE('',#4225,6.0005786784788,5.99999999999999);
#187=ELLIPSE('',#4241,3.00012859866252,3.);
#188=ELLIPSE('',#4244,6.00025719732503,5.99999999999999);
#189=ELLIPSE('',#4246,17.5007501588647,17.5);
#190=ELLIPSE('',#4248,6.00025719732503,5.99999999999999);
#191=ELLIPSE('',#4251,3.00012859866252,3.);
#192=ELLIPSE('',#4255,9.50040722909798,9.5);
#193=TOROIDAL_SURFACE('',#4137,25.,3.);
#194=TOROIDAL_SURFACE('',#4144,32.,3.);
#195=TOROIDAL_SURFACE('',#4150,6.,3.);
#196=TOROIDAL_SURFACE('',#4158,32.,3.);
#197=TOROIDAL_SURFACE('',#4166,25.,3.);
#198=TOROIDAL_SURFACE('',#4173,6.,3.);
#199=TOROIDAL_SURFACE('',#4183,25.,3.);
#200=TOROIDAL_SURFACE('',#4194,25.,3.);
#201=TOROIDAL_SURFACE('',#4212,8.99999999999999,3.);
#202=TOROIDAL_SURFACE('',#4226,8.99999999999999,3.);
#207=B_SPLINE_CURVE_WITH_KNOTS('',3,(#5747,#5748,#5749,#5750),
 .UNSPECIFIED.,.F.,.F.,(4,4),(-0.314873215025081,0.),.UNSPECIFIED.);
#208=B_SPLINE_CURVE_WITH_KNOTS('',3,(#5753,#5754,#5755,#5756),
 .UNSPECIFIED.,.F.,.F.,(4,4),(0.,0.314873215025081),.UNSPECIFIED.);
#209=B_SPLINE_CURVE_WITH_KNOTS('',3,(#5784,#5785,#5786,#5787),
 .UNSPECIFIED.,.F.,.F.,(4,4),(-0.0585005125063144,0.),.UNSPECIFIED.);
#210=B_SPLINE_CURVE_WITH_KNOTS('',3,(#5790,#5791,#5792,#5793),
 .UNSPECIFIED.,.F.,.F.,(4,4),(0.,0.0585005125063144),.UNSPECIFIED.);
#211=B_SPLINE_CURVE_WITH_KNOTS('',3,(#5835,#5836,#5837,#5838,#5839,#5840,
#5841,#5842,#5843,#5844,#5845,#5846,#5847,#5848),.UNSPECIFIED.,.F.,.F.,
(4,2,2,2,2,2,4),(1.81481027575948,1.85509507173471,1.89964280797494,2.0220220083772,
2.21769356951572,2.39982278968484,2.58195200985395),.UNSPECIFIED.);
#212=B_SPLINE_CURVE_WITH_KNOTS('',3,(#5887,#5888,#5889,#5890,#5891,#5892,
#5893,#5894,#5895,#5896,#5897,#5898,#5899,#5900),.UNSPECIFIED.,.F.,.F.,
(4,2,2,2,2,2,4),(4.67728909318397,4.85941831335309,5.04154753352221,5.23721909466073,
5.35959829506298,5.40414603130322,5.44443082727844),.UNSPECIFIED.);
#213=B_SPLINE_CURVE_WITH_KNOTS('',3,(#5933,#5934,#5935,#5936),
 .UNSPECIFIED.,.F.,.F.,(4,4),(-0.31487081906698,0.),.UNSPECIFIED.);
#214=B_SPLINE_CURVE_WITH_KNOTS('',3,(#5938,#5939,#5940,#5941),
 .UNSPECIFIED.,.F.,.F.,(4,4),(0.,0.31487081906698),.UNSPECIFIED.);
#215=B_SPLINE_CURVE_WITH_KNOTS('',3,(#5971,#5972,#5973,#5974),
 .UNSPECIFIED.,.F.,.F.,(4,4),(-0.0585005125063158,0.),.UNSPECIFIED.);
#216=B_SPLINE_CURVE_WITH_KNOTS('',3,(#5975,#5976,#5977,#5978),
 .UNSPECIFIED.,.F.,.F.,(4,4),(0.,0.0585005125063158),.UNSPECIFIED.);
#217=B_SPLINE_CURVE_WITH_KNOTS('',3,(#6078,#6079,#6080,#6081),
 .UNSPECIFIED.,.F.,.F.,(4,4),(-0.0585005125063147,0.),.UNSPECIFIED.);
#218=B_SPLINE_CURVE_WITH_KNOTS('',3,(#6084,#6085,#6086,#6087),
 .UNSPECIFIED.,.F.,.F.,(4,4),(0.,0.0585005125063147),.UNSPECIFIED.);
#219=B_SPLINE_CURVE_WITH_KNOTS('',3,(#6121,#6122,#6123,#6124,#6125,#6126),
 .UNSPECIFIED.,.F.,.F.,(4,2,4),(0.058804296831916,0.150601760228585,0.290945138364171),
 .UNSPECIFIED.);
#220=B_SPLINE_CURVE_WITH_KNOTS('',3,(#6127,#6128,#6129,#6130,#6131),
 .UNSPECIFIED.,.F.,.F.,(4,1,4),(0.937613435458313,0.988925248429188,1.25041151877174),
 .UNSPECIFIED.);
#221=B_SPLINE_CURVE_WITH_KNOTS('',3,(#6133,#6134,#6135,#6136),
 .UNSPECIFIED.,.F.,.F.,(4,4),(-1.25041151877174,-1.10394303083322),
 .UNSPECIFIED.);
#222=B_SPLINE_CURVE_WITH_KNOTS('',3,(#6138,#6139,#6140,#6141,#6142,#6143),
 .UNSPECIFIED.,.F.,.F.,(4,2,4),(-0.00122772925122373,0.,0.0713282894365937),
 .UNSPECIFIED.);
#223=B_SPLINE_CURVE_WITH_KNOTS('',3,(#6144,#6145,#6146,#6147,#6148,#6149),
 .UNSPECIFIED.,.F.,.F.,(4,2,4),(0.104979741457986,0.218385659282761,0.376958276855987),
 .UNSPECIFIED.);
#224=B_SPLINE_CURVE_WITH_KNOTS('',3,(#6160,#6161,#6162,#6163,#6164,#6165),
 .UNSPECIFIED.,.F.,.F.,(4,2,4),(0.377503618079906,0.433661154495474,0.590536904457044),
 .UNSPECIFIED.);
#225=B_SPLINE_CURVE_WITH_KNOTS('',3,(#6168,#6169,#6170,#6171,#6172,#6173),
 .UNSPECIFIED.,.F.,.F.,(4,2,4),(0.100502924090409,0.233024798286911,0.373363044052317),
 .UNSPECIFIED.);
#226=B_SPLINE_CURVE_WITH_KNOTS('',3,(#6233,#6234,#6235,#6236),
 .UNSPECIFIED.,.F.,.F.,(4,4),(-0.0585005125063158,0.),.UNSPECIFIED.);
#227=B_SPLINE_CURVE_WITH_KNOTS('',3,(#6239,#6240,#6241,#6242),
 .UNSPECIFIED.,.F.,.F.,(4,4),(0.,0.0585005125063158),.UNSPECIFIED.);
#228=B_SPLINE_CURVE_WITH_KNOTS('',3,(#6303,#6304,#6305,#6306,#6307,#6308,
#6309,#6310,#6311,#6312,#6313,#6314,#6315),.UNSPECIFIED.,.F.,.F.,(4,3,3,
3,4),(0.395698154007737,0.425905162440753,0.455555657972498,0.466932501158666,
0.468163517607288),.UNSPECIFIED.);
#229=B_SPLINE_CURVE_WITH_KNOTS('',3,(#6316,#6317,#6318,#6319),
 .UNSPECIFIED.,.F.,.F.,(4,4),(1.10577580098667,1.25278641295821),
 .UNSPECIFIED.);
#230=B_SPLINE_CURVE_WITH_KNOTS('',3,(#6321,#6322,#6323,#6324),
 .UNSPECIFIED.,.F.,.F.,(4,4),(-1.25278641295821,-0.938561283624521),
 .UNSPECIFIED.);
#231=B_SPLINE_CURVE_WITH_KNOTS('',3,(#6326,#6327,#6328,#6329,#6330,#6331),
 .UNSPECIFIED.,.F.,.F.,(4,2,4),(0.,0.139148474445525,0.230280439948345),
 .UNSPECIFIED.);
#232=B_SPLINE_CURVE_WITH_KNOTS('',3,(#6332,#6333,#6334,#6335,#6336,#6337),
 .UNSPECIFIED.,.F.,.F.,(4,2,4),(0.0496921589401031,0.160922541821051,0.240485355391862),
 .UNSPECIFIED.);
#233=B_SPLINE_CURVE_WITH_KNOTS('',3,(#6349,#6350,#6351,#6352,#6353,#6354),
 .UNSPECIFIED.,.F.,.F.,(4,2,4),(0.195057093979392,0.323802001349606,0.445376130695255),
 .UNSPECIFIED.);
#234=B_SPLINE_CURVE_WITH_KNOTS('',3,(#6384,#6385,#6386,#6387,#6388,#6389),
 .UNSPECIFIED.,.F.,.F.,(4,2,4),(0.,0.143083785469884,0.194304148687177),
 .UNSPECIFIED.);
#235=B_SPLINE_CURVE_WITH_KNOTS('',3,(#6407,#6408,#6409,#6410,#6411,#6412,
#6413,#6414,#6415,#6416,#6417,#6418),.UNSPECIFIED.,.F.,.F.,(4,2,2,2,2,4),
(-0.0021944909380558,0.,0.118954781425746,0.236148568198992,0.353341240908116,
0.470533846489538),.UNSPECIFIED.);
#236=B_SPLINE_CURVE_WITH_KNOTS('',3,(#6451,#6452,#6453,#6454,#6455,#6456,
#6457),.UNSPECIFIED.,.F.,.F.,(4,3,4),(-0.537933556304323,-0.536871151957347,
-0.536116003149211),.UNSPECIFIED.);
#237=B_SPLINE_CURVE_WITH_KNOTS('',3,(#6538,#6539,#6540,#6541,#6542,#6543,
#6544,#6545,#6546,#6547,#6548,#6549,#6550,#6551,#6552,#6553,#6554,#6555,
#6556,#6557,#6558,#6559,#6560,#6561,#6562,#6563,#6564,#6565,#6566,#6567,
#6568,#6569,#6570,#6571,#6572,#6573,#6574,#6575,#6576,#6577,#6578,#6579,
#6580,#6581,#6582,#6583,#6584,#6585,#6586,#6587,#6588,#6589,#6590,#6591,
#6592),.UNSPECIFIED.,.F.,.F.,(4,3,3,3,3,3,3,3,3,3,3,3,3,3,3,3,3,3,4),(-0.472728188530224,
-0.470533698488276,-0.440746367412676,-0.410416837256165,-0.379701952247477,
-0.351578951638149,-0.320921325925665,-0.290206141350092,-0.260036055125886,
-0.234385204179885,-0.203800840065922,-0.201744974296049,-0.171564828698904,
-0.141015529658378,-0.117192569025982,-0.0867072980072964,-0.0561496264825006,
-0.0261504853702348,0.),.UNSPECIFIED.);
#238=B_SPLINE_CURVE_WITH_KNOTS('',3,(#6593,#6594,#6595,#6596,#6597,#6598,
#6599),.UNSPECIFIED.,.F.,.F.,(4,3,4),(-0.00165554359406403,-0.00116998025873546,
0.),.UNSPECIFIED.);
#300=B_SPLINE_SURFACE_WITH_KNOTS('',3,3,((#5724,#5725,#5726,#5727),(#5728,
#5729,#5730,#5731),(#5732,#5733,#5734,#5735),(#5736,#5737,#5738,#5739),
(#5740,#5741,#5742,#5743)),.UNSPECIFIED.,.F.,.F.,.F.,(4,1,4),(4,4),(0.,
0.571428571428571,1.),(0.,0.314873215025081),.UNSPECIFIED.);
#301=B_SPLINE_SURFACE_WITH_KNOTS('',3,3,((#5763,#5764,#5765,#5766),(#5767,
#5768,#5769,#5770),(#5771,#5772,#5773,#5774),(#5775,#5776,#5777,#5778),
(#5779,#5780,#5781,#5782)),.UNSPECIFIED.,.F.,.F.,.F.,(4,1,4),(4,4),(0.,
0.571428571428571,1.),(0.,0.0585005125063144),.UNSPECIFIED.);
#302=B_SPLINE_SURFACE_WITH_KNOTS('',3,3,((#5794,#5795,#5796,#5797,#5798,
#5799,#5800),(#5801,#5802,#5803,#5804,#5805,#5806,#5807),(#5808,#5809,#5810,
#5811,#5812,#5813,#5814),(#5815,#5816,#5817,#5818,#5819,#5820,#5821),(#5822,
#5823,#5824,#5825,#5826,#5827,#5828)),.UNSPECIFIED.,.F.,.F.,.F.,(4,1,4),
(4,1,1,1,4),(0.,0.571428571428571,1.),(0.0969258860400105,0.307478806147851,
0.728584646363533,1.14969048657921,1.5707963267949),.UNSPECIFIED.);
#303=B_SPLINE_SURFACE_WITH_KNOTS('',3,3,((#5909,#5910,#5911,#5912),(#5913,
#5914,#5915,#5916),(#5917,#5918,#5919,#5920),(#5921,#5922,#5923,#5924),
(#5925,#5926,#5927,#5928)),.UNSPECIFIED.,.F.,.F.,.F.,(4,1,4),(4,4),(0.,
0.571428571428571,1.),(0.,0.31487081906698),.UNSPECIFIED.);
#304=B_SPLINE_SURFACE_WITH_KNOTS('',3,3,((#5948,#5949,#5950,#5951),(#5952,
#5953,#5954,#5955),(#5956,#5957,#5958,#5959),(#5960,#5961,#5962,#5963),
(#5964,#5965,#5966,#5967)),.UNSPECIFIED.,.F.,.F.,.F.,(4,1,4),(4,4),(0.,
0.571428571428571,1.),(0.,0.0585005125063158),.UNSPECIFIED.);
#305=B_SPLINE_SURFACE_WITH_KNOTS('',3,3,((#5979,#5980,#5981,#5982,#5983,
#5984),(#5985,#5986,#5987,#5988,#5989,#5990),(#5991,#5992,#5993,#5994,#5995,
#5996),(#5997,#5998,#5999,#6000,#6001,#6002),(#6003,#6004,#6005,#6006,#6007,
#6008)),.UNSPECIFIED.,.F.,.F.,.F.,(4,1,4),(4,1,1,4),(0.,0.571428571428571,
1.),(-1.5707963267949,-0.939137566471373,-0.518031726255691,-0.0969258860400086),
 .UNSPECIFIED.);
#306=B_SPLINE_SURFACE_WITH_KNOTS('',3,3,((#6022,#6023,#6024,#6025,#6026,
#6027),(#6028,#6029,#6030,#6031,#6032,#6033),(#6034,#6035,#6036,#6037,#6038,
#6039),(#6040,#6041,#6042,#6043,#6044,#6045),(#6046,#6047,#6048,#6049,#6050,
#6051)),.UNSPECIFIED.,.F.,.F.,.F.,(4,1,4),(4,1,1,4),(0.,0.571428571428571,
1.),(-1.5707963267949,-0.939137566471373,-0.51803172625569,-0.0969258860400074),
 .UNSPECIFIED.);
#307=B_SPLINE_SURFACE_WITH_KNOTS('',3,3,((#6057,#6058,#6059,#6060),(#6061,
#6062,#6063,#6064),(#6065,#6066,#6067,#6068),(#6069,#6070,#6071,#6072),
(#6073,#6074,#6075,#6076)),.UNSPECIFIED.,.F.,.F.,.F.,(4,1,4),(4,4),(0.,
0.571428571428571,1.),(0.,0.0585005125063147),.UNSPECIFIED.);
#308=B_SPLINE_SURFACE_WITH_KNOTS('',3,3,((#6094,#6095,#6096,#6097,#6098),
(#6099,#6100,#6101,#6102,#6103),(#6104,#6105,#6106,#6107,#6108),(#6109,
#6110,#6111,#6112,#6113),(#6114,#6115,#6116,#6117,#6118)),.UNSPECIFIED.,
 .F.,.F.,.F.,(4,1,4),(4,1,4),(0.,0.571428571428571,1.),(0.792810545672275,
0.988925248429188,1.25041151877174),.UNSPECIFIED.);
#309=B_SPLINE_SURFACE_WITH_KNOTS('',3,3,((#6174,#6175,#6176,#6177,#6178),
(#6179,#6180,#6181,#6182,#6183),(#6184,#6185,#6186,#6187,#6188),(#6189,
#6190,#6191,#6192,#6193),(#6194,#6195,#6196,#6197,#6198)),.UNSPECIFIED.,
 .F.,.F.,.F.,(4,1,4),(4,1,4),(0.,0.571428571428571,1.),(-1.5707963267949,
-0.999178609866638,-0.237021653962293),.UNSPECIFIED.);
#310=B_SPLINE_SURFACE_WITH_KNOTS('',3,3,((#6212,#6213,#6214,#6215),(#6216,
#6217,#6218,#6219),(#6220,#6221,#6222,#6223),(#6224,#6225,#6226,#6227),
(#6228,#6229,#6230,#6231)),.UNSPECIFIED.,.F.,.F.,.F.,(4,1,4),(4,4),(0.,
0.571428571428571,1.),(0.,0.0585005125063158),.UNSPECIFIED.);
#311=B_SPLINE_SURFACE_WITH_KNOTS('',3,3,((#6243,#6244,#6245,#6246,#6247,
#6248,#6249),(#6250,#6251,#6252,#6253,#6254,#6255,#6256),(#6257,#6258,#6259,
#6260,#6261,#6262,#6263),(#6264,#6265,#6266,#6267,#6268,#6269,#6270),(#6271,
#6272,#6273,#6274,#6275,#6276,#6277)),.UNSPECIFIED.,.F.,.F.,.F.,(4,1,4),
(4,1,1,1,4),(0.,0.571428571428571,1.),(0.0969258860400078,0.307478806147849,
0.728584646363532,1.14969048657921,1.5707963267949),.UNSPECIFIED.);
#312=B_SPLINE_SURFACE_WITH_KNOTS('',3,3,((#6281,#6282,#6283,#6284),(#6285,
#6286,#6287,#6288),(#6289,#6290,#6291,#6292),(#6293,#6294,#6295,#6296),
(#6297,#6298,#6299,#6300)),.UNSPECIFIED.,.F.,.F.,.F.,(4,1,4),(4,4),(0.,
0.571428571428571,1.),(0.793286355786688,1.25278641295821),
 .UNSPECIFIED.);
#313=B_SPLINE_SURFACE_WITH_KNOTS('',3,3,((#6358,#6359,#6360,#6361,#6362),
(#6363,#6364,#6365,#6366,#6367),(#6368,#6369,#6370,#6371,#6372),(#6373,
#6374,#6375,#6376,#6377),(#6378,#6379,#6380,#6381,#6382)),.UNSPECIFIED.,
 .F.,.F.,.F.,(4,1,4),(4,1,4),(0.,0.571428571428571,1.),(-1.5707963267949,
-0.99917860986662,-0.23702165396225),.UNSPECIFIED.);
#314=B_SPLINE_SURFACE_WITH_KNOTS('',3,3,((#6425,#6426,#6427,#6428),(#6429,
#6430,#6431,#6432),(#6433,#6434,#6435,#6436),(#6437,#6438,#6439,#6440),
(#6441,#6442,#6443,#6444)),.UNSPECIFIED.,.F.,.F.,.F.,(4,1,4),(4,4),(0.,
0.571428571428571,1.),(0.98361909310298,1.35639146206056),.UNSPECIFIED.);
#315=B_SPLINE_SURFACE_WITH_KNOTS('',3,3,((#6458,#6459,#6460,#6461,#6462,
#6463,#6464,#6465,#6466,#6467),(#6468,#6469,#6470,#6471,#6472,#6473,#6474,
#6475,#6476,#6477),(#6478,#6479,#6480,#6481,#6482,#6483,#6484,#6485,#6486,
#6487),(#6488,#6489,#6490,#6491,#6492,#6493,#6494,#6495,#6496,#6497),(#6498,
#6499,#6500,#6501,#6502,#6503,#6504,#6505,#6506,#6507)),.UNSPECIFIED.,.F.,
 .F.,.F.,(4,1,4),(4,1,1,1,1,1,1,4),(0.,0.571428571428571,1.),(-1.35639146206079,
-0.968851044329184,-0.581310626597581,-0.193770208865978,0.193770208865625,
0.581310626597229,0.968851044328832,1.35639146206044),.UNSPECIFIED.);
#316=B_SPLINE_SURFACE_WITH_KNOTS('',3,3,((#6513,#6514,#6515,#6516),(#6517,
#6518,#6519,#6520),(#6521,#6522,#6523,#6524),(#6525,#6526,#6527,#6528),
(#6529,#6530,#6531,#6532)),.UNSPECIFIED.,.F.,.F.,.F.,(4,1,4),(4,4),(0.,
0.571428571428571,1.),(4.92679384511897,5.29956633635466),.UNSPECIFIED.);
#337=FACE_BOUND('',#770,.T.);
#338=FACE_BOUND('',#771,.T.);
#339=FACE_BOUND('',#775,.T.);
#340=FACE_BOUND('',#776,.T.);
#341=FACE_BOUND('',#786,.T.);
#342=FACE_BOUND('',#797,.T.);
#343=FACE_BOUND('',#816,.T.);
#344=FACE_BOUND('',#839,.T.);
#345=FACE_BOUND('',#845,.T.);
#346=FACE_BOUND('',#861,.T.);
#347=FACE_BOUND('',#862,.T.);
#369=CIRCLE('',#4122,3.);
#370=CIRCLE('',#4123,3.);
#371=CIRCLE('',#4126,6.);
#372=CIRCLE('',#4127,6.);
#373=CIRCLE('',#4129,28.);
#374=CIRCLE('',#4130,3.);
#375=CIRCLE('',#4131,3.);
#376=CIRCLE('',#4132,28.);
#377=CIRCLE('',#4133,4.);
#378=CIRCLE('',#4134,3.99999999999999);
#379=CIRCLE('',#4135,3.);
#380=CIRCLE('',#4136,3.);
#381=CIRCLE('',#4138,3.);
#382=CIRCLE('',#4139,28.);
#383=CIRCLE('',#4140,25.);
#384=CIRCLE('',#4141,3.);
#385=CIRCLE('',#4145,32.);
#386=CIRCLE('',#4146,3.);
#387=CIRCLE('',#4147,35.);
#388=CIRCLE('',#4149,3.);
#389=CIRCLE('',#4151,3.);
#390=CIRCLE('',#4153,3.);
#391=CIRCLE('',#4155,4.);
#392=CIRCLE('',#4159,35.);
#393=CIRCLE('',#4160,3.);
#394=CIRCLE('',#4161,32.);
#395=CIRCLE('',#4163,3.);
#396=CIRCLE('',#4164,3.);
#397=CIRCLE('',#4165,3.);
#398=CIRCLE('',#4167,3.00000000000001);
#399=CIRCLE('',#4168,25.);
#400=CIRCLE('',#4169,28.);
#401=CIRCLE('',#4170,3.);
#402=CIRCLE('',#4174,3.);
#403=CIRCLE('',#4176,4.);
#404=CIRCLE('',#4179,3.);
#405=CIRCLE('',#4182,3.);
#406=CIRCLE('',#4184,3.);
#407=CIRCLE('',#4185,28.);
#408=CIRCLE('',#4186,25.);
#409=CIRCLE('',#4188,28.);
#410=CIRCLE('',#4192,3.00000000000002);
#411=CIRCLE('',#4195,3.);
#412=CIRCLE('',#4196,28.);
#413=CIRCLE('',#4197,2.99999999999997);
#414=CIRCLE('',#4198,25.);
#415=CIRCLE('',#4199,3.);
#416=CIRCLE('',#4207,3.99999999999999);
#417=CIRCLE('',#4209,3.);
#418=CIRCLE('',#4211,3.00000000000002);
#419=CIRCLE('',#4213,8.99999999999999);
#420=CIRCLE('',#4214,3.00000000000002);
#421=CIRCLE('',#4215,5.99999999999999);
#422=CIRCLE('',#4217,3.00000000000005);
#423=CIRCLE('',#4219,3.);
#424=CIRCLE('',#4221,3.);
#425=CIRCLE('',#4227,5.99999999999999);
#426=CIRCLE('',#4228,3.);
#427=CIRCLE('',#4229,8.99999999999999);
#428=CIRCLE('',#4231,3.);
#429=CIRCLE('',#4233,3.);
#430=CIRCLE('',#4235,3.);
#431=CIRCLE('',#4237,3.);
#432=CIRCLE('',#4253,9.5);
#433=CIRCLE('',#4256,9.5);
#434=CIRCLE('',#4259,3.);
#435=CIRCLE('',#4262,3.99999999999999);
#436=CIRCLE('',#4265,4.);
#437=CIRCLE('',#4267,28.);
#438=CIRCLE('',#4270,3.99999999999999);
#439=CIRCLE('',#4274,3.);
#440=CIRCLE('',#4277,3.);
#526=FACE_OUTER_BOUND('',#761,.T.);
#527=FACE_OUTER_BOUND('',#762,.T.);
#528=FACE_OUTER_BOUND('',#763,.T.);
#529=FACE_OUTER_BOUND('',#764,.T.);
#530=FACE_OUTER_BOUND('',#765,.T.);
#531=FACE_OUTER_BOUND('',#766,.T.);
#532=FACE_OUTER_BOUND('',#767,.T.);
#533=FACE_OUTER_BOUND('',#768,.T.);
#534=FACE_OUTER_BOUND('',#769,.T.);
#535=FACE_OUTER_BOUND('',#772,.T.);
#536=FACE_OUTER_BOUND('',#773,.T.);
#537=FACE_OUTER_BOUND('',#774,.T.);
#538=FACE_OUTER_BOUND('',#777,.T.);
#539=FACE_OUTER_BOUND('',#778,.T.);
#540=FACE_OUTER_BOUND('',#779,.T.);
#541=FACE_OUTER_BOUND('',#780,.T.);
#542=FACE_OUTER_BOUND('',#781,.T.);
#543=FACE_OUTER_BOUND('',#782,.T.);
#544=FACE_OUTER_BOUND('',#783,.T.);
#545=FACE_OUTER_BOUND('',#784,.T.);
#546=FACE_OUTER_BOUND('',#785,.T.);
#547=FACE_OUTER_BOUND('',#787,.T.);
#548=FACE_OUTER_BOUND('',#788,.T.);
#549=FACE_OUTER_BOUND('',#789,.T.);
#550=FACE_OUTER_BOUND('',#790,.T.);
#551=FACE_OUTER_BOUND('',#791,.T.);
#552=FACE_OUTER_BOUND('',#792,.T.);
#553=FACE_OUTER_BOUND('',#793,.T.);
#554=FACE_OUTER_BOUND('',#794,.T.);
#555=FACE_OUTER_BOUND('',#795,.T.);
#556=FACE_OUTER_BOUND('',#796,.T.);
#557=FACE_OUTER_BOUND('',#798,.T.);
#558=FACE_OUTER_BOUND('',#799,.T.);
#559=FACE_OUTER_BOUND('',#800,.T.);
#560=FACE_OUTER_BOUND('',#801,.T.);
#561=FACE_OUTER_BOUND('',#802,.T.);
#562=FACE_OUTER_BOUND('',#803,.T.);
#563=FACE_OUTER_BOUND('',#804,.T.);
#564=FACE_OUTER_BOUND('',#805,.T.);
#565=FACE_OUTER_BOUND('',#806,.T.);
#566=FACE_OUTER_BOUND('',#807,.T.);
#567=FACE_OUTER_BOUND('',#808,.T.);
#568=FACE_OUTER_BOUND('',#809,.T.);
#569=FACE_OUTER_BOUND('',#810,.T.);
#570=FACE_OUTER_BOUND('',#811,.T.);
#571=FACE_OUTER_BOUND('',#812,.T.);
#572=FACE_OUTER_BOUND('',#813,.T.);
#573=FACE_OUTER_BOUND('',#814,.T.);
#574=FACE_OUTER_BOUND('',#815,.T.);
#575=FACE_OUTER_BOUND('',#817,.T.);
#576=FACE_OUTER_BOUND('',#818,.T.);
#577=FACE_OUTER_BOUND('',#819,.T.);
#578=FACE_OUTER_BOUND('',#820,.T.);
#579=FACE_OUTER_BOUND('',#821,.T.);
#580=FACE_OUTER_BOUND('',#822,.T.);
#581=FACE_OUTER_BOUND('',#823,.T.);
#582=FACE_OUTER_BOUND('',#824,.T.);
#583=FACE_OUTER_BOUND('',#825,.T.);
#584=FACE_OUTER_BOUND('',#826,.T.);
#585=FACE_OUTER_BOUND('',#827,.T.);
#586=FACE_OUTER_BOUND('',#828,.T.);
#587=FACE_OUTER_BOUND('',#829,.T.);
#588=FACE_OUTER_BOUND('',#830,.T.);
#589=FACE_OUTER_BOUND('',#831,.T.);
#590=FACE_OUTER_BOUND('',#832,.T.);
#591=FACE_OUTER_BOUND('',#833,.T.);
#592=FACE_OUTER_BOUND('',#834,.T.);
#593=FACE_OUTER_BOUND('',#835,.T.);
#594=FACE_OUTER_BOUND('',#836,.T.);
#595=FACE_OUTER_BOUND('',#837,.T.);
#596=FACE_OUTER_BOUND('',#838,.T.);
#597=FACE_OUTER_BOUND('',#840,.T.);
#598=FACE_OUTER_BOUND('',#841,.T.);
#599=FACE_OUTER_BOUND('',#842,.T.);
#600=FACE_OUTER_BOUND('',#843,.T.);
#601=FACE_OUTER_BOUND('',#844,.T.);
#602=FACE_OUTER_BOUND('',#846,.T.);
#603=FACE_OUTER_BOUND('',#847,.T.);
#604=FACE_OUTER_BOUND('',#848,.T.);
#605=FACE_OUTER_BOUND('',#849,.T.);
#606=FACE_OUTER_BOUND('',#850,.T.);
#607=FACE_OUTER_BOUND('',#851,.T.);
#608=FACE_OUTER_BOUND('',#852,.T.);
#609=FACE_OUTER_BOUND('',#853,.T.);
#610=FACE_OUTER_BOUND('',#854,.T.);
#611=FACE_OUTER_BOUND('',#855,.T.);
#612=FACE_OUTER_BOUND('',#856,.T.);
#613=FACE_OUTER_BOUND('',#857,.T.);
#614=FACE_OUTER_BOUND('',#858,.T.);
#615=FACE_OUTER_BOUND('',#859,.T.);
#616=FACE_OUTER_BOUND('',#860,.T.);
#617=FACE_OUTER_BOUND('',#863,.T.);
#761=EDGE_LOOP('',(#2527,#2528,#2529,#2530));
#762=EDGE_LOOP('',(#2531,#2532,#2533,#2534));
#763=EDGE_LOOP('',(#2535,#2536,#2537,#2538));
#764=EDGE_LOOP('',(#2539,#2540,#2541,#2542));
#765=EDGE_LOOP('',(#2543,#2544,#2545,#2546,#2547,#2548,#2549,#2550));
#766=EDGE_LOOP('',(#2551,#2552,#2553,#2554));
#767=EDGE_LOOP('',(#2555,#2556,#2557,#2558,#2559,#2560,#2561,#2562));
#768=EDGE_LOOP('',(#2563,#2564,#2565,#2566));
#769=EDGE_LOOP('',(#2567,#2568,#2569,#2570,#2571,#2572,#2573,#2574));
#770=EDGE_LOOP('',(#2575));
#771=EDGE_LOOP('',(#2576));
#772=EDGE_LOOP('',(#2577,#2578,#2579,#2580));
#773=EDGE_LOOP('',(#2581,#2582,#2583,#2584,#2585,#2586,#2587,#2588,#2589,
#2590,#2591,#2592,#2593,#2594,#2595,#2596));
#774=EDGE_LOOP('',(#2597,#2598,#2599,#2600,#2601,#2602,#2603,#2604));
#775=EDGE_LOOP('',(#2605));
#776=EDGE_LOOP('',(#2606));
#777=EDGE_LOOP('',(#2607,#2608,#2609,#2610));
#778=EDGE_LOOP('',(#2611,#2612,#2613,#2614));
#779=EDGE_LOOP('',(#2615,#2616,#2617,#2618));
#780=EDGE_LOOP('',(#2619,#2620,#2621));
#781=EDGE_LOOP('',(#2622,#2623,#2624,#2625));
#782=EDGE_LOOP('',(#2626,#2627,#2628,#2629));
#783=EDGE_LOOP('',(#2630,#2631,#2632,#2633));
#784=EDGE_LOOP('',(#2634,#2635,#2636,#2637));
#785=EDGE_LOOP('',(#2638,#2639));
#786=EDGE_LOOP('',(#2640));
#787=EDGE_LOOP('',(#2641,#2642,#2643,#2644,#2645,#2646));
#788=EDGE_LOOP('',(#2647,#2648,#2649,#2650,#2651,#2652,#2653,#2654,#2655,
#2656,#2657,#2658,#2659));
#789=EDGE_LOOP('',(#2660,#2661,#2662,#2663));
#790=EDGE_LOOP('',(#2664,#2665,#2666,#2667));
#791=EDGE_LOOP('',(#2668,#2669,#2670,#2671));
#792=EDGE_LOOP('',(#2672,#2673,#2674,#2675));
#793=EDGE_LOOP('',(#2676,#2677,#2678,#2679));
#794=EDGE_LOOP('',(#2680,#2681,#2682));
#795=EDGE_LOOP('',(#2683,#2684,#2685,#2686));
#796=EDGE_LOOP('',(#2687,#2688));
#797=EDGE_LOOP('',(#2689));
#798=EDGE_LOOP('',(#2690,#2691,#2692,#2693));
#799=EDGE_LOOP('',(#2694,#2695,#2696,#2697,#2698,#2699));
#800=EDGE_LOOP('',(#2700,#2701,#2702));
#801=EDGE_LOOP('',(#2703,#2704,#2705,#2706));
#802=EDGE_LOOP('',(#2707,#2708,#2709,#2710));
#803=EDGE_LOOP('',(#2711,#2712,#2713,#2714,#2715,#2716));
#804=EDGE_LOOP('',(#2717,#2718,#2719,#2720,#2721,#2722));
#805=EDGE_LOOP('',(#2723,#2724,#2725,#2726,#2727));
#806=EDGE_LOOP('',(#2728,#2729,#2730));
#807=EDGE_LOOP('',(#2731,#2732,#2733,#2734,#2735,#2736));
#808=EDGE_LOOP('',(#2737,#2738,#2739,#2740));
#809=EDGE_LOOP('',(#2741,#2742,#2743,#2744));
#810=EDGE_LOOP('',(#2745,#2746,#2747));
#811=EDGE_LOOP('',(#2748,#2749,#2750,#2751,#2752,#2753));
#812=EDGE_LOOP('',(#2754,#2755,#2756,#2757));
#813=EDGE_LOOP('',(#2758,#2759,#2760,#2761,#2762,#2763));
#814=EDGE_LOOP('',(#2764,#2765,#2766));
#815=EDGE_LOOP('',(#2767,#2768));
#816=EDGE_LOOP('',(#2769));
#817=EDGE_LOOP('',(#2770,#2771,#2772,#2773,#2774,#2775));
#818=EDGE_LOOP('',(#2776,#2777,#2778,#2779));
#819=EDGE_LOOP('',(#2780,#2781,#2782,#2783));
#820=EDGE_LOOP('',(#2784,#2785,#2786,#2787));
#821=EDGE_LOOP('',(#2788,#2789,#2790,#2791,#2792));
#822=EDGE_LOOP('',(#2793,#2794,#2795,#2796));
#823=EDGE_LOOP('',(#2797,#2798,#2799,#2800,#2801));
#824=EDGE_LOOP('',(#2802,#2803,#2804,#2805));
#825=EDGE_LOOP('',(#2806,#2807,#2808,#2809));
#826=EDGE_LOOP('',(#2810,#2811,#2812,#2813));
#827=EDGE_LOOP('',(#2814,#2815,#2816));
#828=EDGE_LOOP('',(#2817,#2818,#2819));
#829=EDGE_LOOP('',(#2820,#2821,#2822,#2823,#2824,#2825));
#830=EDGE_LOOP('',(#2826,#2827,#2828,#2829,#2830,#2831,#2832,#2833,#2834,
#2835,#2836,#2837,#2838));
#831=EDGE_LOOP('',(#2839,#2840,#2841,#2842));
#832=EDGE_LOOP('',(#2843,#2844,#2845,#2846));
#833=EDGE_LOOP('',(#2847,#2848,#2849,#2850,#2851));
#834=EDGE_LOOP('',(#2852,#2853,#2854,#2855));
#835=EDGE_LOOP('',(#2856,#2857,#2858,#2859,#2860));
#836=EDGE_LOOP('',(#2861,#2862,#2863,#2864));
#837=EDGE_LOOP('',(#2865,#2866,#2867,#2868));
#838=EDGE_LOOP('',(#2869,#2870,#2871,#2872,#2873,#2874,#2875,#2876,#2877,
#2878,#2879,#2880,#2881,#2882));
#839=EDGE_LOOP('',(#2883));
#840=EDGE_LOOP('',(#2884,#2885,#2886,#2887,#2888));
#841=EDGE_LOOP('',(#2889,#2890,#2891,#2892,#2893,#2894));
#842=EDGE_LOOP('',(#2895,#2896,#2897,#2898));
#843=EDGE_LOOP('',(#2899,#2900,#2901,#2902,#2903,#2904));
#844=EDGE_LOOP('',(#2905,#2906));
#845=EDGE_LOOP('',(#2907));
#846=EDGE_LOOP('',(#2908,#2909,#2910,#2911,#2912,#2913));
#847=EDGE_LOOP('',(#2914,#2915,#2916,#2917));
#848=EDGE_LOOP('',(#2918,#2919,#2920,#2921,#2922,#2923));
#849=EDGE_LOOP('',(#2924,#2925,#2926,#2927));
#850=EDGE_LOOP('',(#2928,#2929,#2930,#2931));
#851=EDGE_LOOP('',(#2932,#2933,#2934,#2935));
#852=EDGE_LOOP('',(#2936,#2937,#2938,#2939,#2940));
#853=EDGE_LOOP('',(#2941,#2942,#2943));
#854=EDGE_LOOP('',(#2944,#2945,#2946,#2947));
#855=EDGE_LOOP('',(#2948,#2949,#2950));
#856=EDGE_LOOP('',(#2951,#2952,#2953,#2954));
#857=EDGE_LOOP('',(#2955,#2956,#2957,#2958));
#858=EDGE_LOOP('',(#2959,#2960,#2961,#2962,#2963,#2964));
#859=EDGE_LOOP('',(#2965,#2966,#2967,#2968));
#860=EDGE_LOOP('',(#2969,#2970,#2971,#2972,#2973,#2974,#2975,#2976));
#861=EDGE_LOOP('',(#2977));
#862=EDGE_LOOP('',(#2978));
#863=EDGE_LOOP('',(#2979,#2980,#2981,#2982,#2983,#2984,#2985,#2986,#2987,
#2988,#2989,#2990,#2991,#2992,#2993,#2994,#2995,#2996,#2997,#2998,#2999,
#3000,#3001,#3002));
#1028=LINE('',#5611,#1317);
#1029=LINE('',#5613,#1318);
#1030=LINE('',#5615,#1319);
#1031=LINE('',#5616,#1320);
#1032=LINE('',#5619,#1321);
#1033=LINE('',#5621,#1322);
#1034=LINE('',#5622,#1323);
#1035=LINE('',#5626,#1324);
#1036=LINE('',#5628,#1325);
#1037=LINE('',#5630,#1326);
#1038=LINE('',#5631,#1327);
#1039=LINE('',#5635,#1328);
#1040=LINE('',#5637,#1329);
#1041=LINE('',#5639,#1330);
#1042=LINE('',#5640,#1331);
#1043=LINE('',#5643,#1332);
#1044=LINE('',#5645,#1333);
#1045=LINE('',#5647,#1334);
#1046=LINE('',#5649,#1335);
#1047=LINE('',#5650,#1336);
#1048=LINE('',#5651,#1337);
#1049=LINE('',#5654,#1338);
#1050=LINE('',#5656,#1339);
#1051=LINE('',#5657,#1340);
#1052=LINE('',#5660,#1341);
#1053=LINE('',#5661,#1342);
#1054=LINE('',#5663,#1343);
#1055=LINE('',#5665,#1344);
#1056=LINE('',#5667,#1345);
#1057=LINE('',#5668,#1346);
#1058=LINE('',#5670,#1347);
#1059=LINE('',#5671,#1348);
#1060=LINE('',#5674,#1349);
#1061=LINE('',#5676,#1350);
#1062=LINE('',#5678,#1351);
#1063=LINE('',#5680,#1352);
#1064=LINE('',#5681,#1353);
#1065=LINE('',#5688,#1354);
#1066=LINE('',#5689,#1355);
#1067=LINE('',#5692,#1356);
#1068=LINE('',#5694,#1357);
#1069=LINE('',#5698,#1358);
#1070=LINE('',#5700,#1359);
#1071=LINE('',#5702,#1360);
#1072=LINE('',#5706,#1361);
#1073=LINE('',#5707,#1362);
#1074=LINE('',#5710,#1363);
#1075=LINE('',#5716,#1364);
#1076=LINE('',#5856,#1365);
#1077=LINE('',#5861,#1366);
#1078=LINE('',#5864,#1367);
#1079=LINE('',#5866,#1368);
#1080=LINE('',#5870,#1369);
#1081=LINE('',#5872,#1370);
#1082=LINE('',#5874,#1371);
#1083=LINE('',#5876,#1372);
#1084=LINE('',#5878,#1373);
#1085=LINE('',#5880,#1374);
#1086=LINE('',#5882,#1375);
#1087=LINE('',#5883,#1376);
#1088=LINE('',#5908,#1377);
#1089=LINE('',#6015,#1378);
#1090=LINE('',#6019,#1379);
#1091=LINE('',#6020,#1380);
#1092=LINE('',#6152,#1381);
#1093=LINE('',#6155,#1382);
#1094=LINE('',#6158,#1383);
#1095=LINE('',#6166,#1384);
#1096=LINE('',#6339,#1385);
#1097=LINE('',#6340,#1386);
#1098=LINE('',#6342,#1387);
#1099=LINE('',#6345,#1388);
#1100=LINE('',#6348,#1389);
#1101=LINE('',#6395,#1390);
#1102=LINE('',#6398,#1391);
#1103=LINE('',#6423,#1392);
#1104=LINE('',#6424,#1393);
#1105=LINE('',#6609,#1394);
#1106=LINE('',#6610,#1395);
#1107=LINE('',#6613,#1396);
#1108=LINE('',#6619,#1397);
#1109=LINE('',#6621,#1398);
#1110=LINE('',#6623,#1399);
#1111=LINE('',#6625,#1400);
#1112=LINE('',#6626,#1401);
#1113=LINE('',#6627,#1402);
#1114=LINE('',#6630,#1403);
#1115=LINE('',#6634,#1404);
#1116=LINE('',#6635,#1405);
#1117=LINE('',#6638,#1406);
#1118=LINE('',#6642,#1407);
#1119=LINE('',#6646,#1408);
#1120=LINE('',#6650,#1409);
#1121=LINE('',#6651,#1410);
#1122=LINE('',#6655,#1411);
#1123=LINE('',#6663,#1412);
#1124=LINE('',#6665,#1413);
#1125=LINE('',#6666,#1414);
#1126=LINE('',#6670,#1415);
#1127=LINE('',#6677,#1416);
#1128=LINE('',#6682,#1417);
#1129=LINE('',#6685,#1418);
#1130=LINE('',#6688,#1419);
#1131=LINE('',#6690,#1420);
#1132=LINE('',#6695,#1421);
#1133=LINE('',#6697,#1422);
#1134=LINE('',#6702,#1423);
#1135=LINE('',#6704,#1424);
#1136=LINE('',#6707,#1425);
#1137=LINE('',#6710,#1426);
#1317=VECTOR('',#4519,10.);
#1318=VECTOR('',#4520,10.);
#1319=VECTOR('',#4521,10.);
#1320=VECTOR('',#4522,10.);
#1321=VECTOR('',#4525,10.);
#1322=VECTOR('',#4526,10.);
#1323=VECTOR('',#4527,10.);
#1324=VECTOR('',#4530,10.);
#1325=VECTOR('',#4531,10.);
#1326=VECTOR('',#4532,10.);
#1327=VECTOR('',#4533,10.);
#1328=VECTOR('',#4536,10.);
#1329=VECTOR('',#4537,10.);
#1330=VECTOR('',#4538,10.);
#1331=VECTOR('',#4539,10.);
#1332=VECTOR('',#4542,10.);
#1333=VECTOR('',#4543,10.);
#1334=VECTOR('',#4544,10.);
#1335=VECTOR('',#4545,10.);
#1336=VECTOR('',#4546,10.);
#1337=VECTOR('',#4547,10.);
#1338=VECTOR('',#4550,10.);
#1339=VECTOR('',#4551,10.);
#1340=VECTOR('',#4552,10.);
#1341=VECTOR('',#4555,10.);
#1342=VECTOR('',#4556,10.);
#1343=VECTOR('',#4557,10.);
#1344=VECTOR('',#4558,10.);
#1345=VECTOR('',#4559,10.);
#1346=VECTOR('',#4560,10.);
#1347=VECTOR('',#4563,10.);
#1348=VECTOR('',#4564,10.);
#1349=VECTOR('',#4567,10.);
#1350=VECTOR('',#4568,10.);
#1351=VECTOR('',#4569,10.);
#1352=VECTOR('',#4570,10.);
#1353=VECTOR('',#4571,10.);
#1354=VECTOR('',#4578,10.);
#1355=VECTOR('',#4579,10.);
#1356=VECTOR('',#4582,10.);
#1357=VECTOR('',#4583,10.);
#1358=VECTOR('',#4586,10.);
#1359=VECTOR('',#4587,10.);
#1360=VECTOR('',#4588,10.);
#1361=VECTOR('',#4591,10.);
#1362=VECTOR('',#4592,10.);
#1363=VECTOR('',#4595,10.);
#1364=VECTOR('',#4600,10.);
#1365=VECTOR('',#4639,10.);
#1366=VECTOR('',#4646,10.);
#1367=VECTOR('',#4649,10.);
#1368=VECTOR('',#4652,10.);
#1369=VECTOR('',#4657,10.);
#1370=VECTOR('',#4660,10.);
#1371=VECTOR('',#4661,10.);
#1372=VECTOR('',#4662,10.);
#1373=VECTOR('',#4663,10.);
#1374=VECTOR('',#4664,10.);
#1375=VECTOR('',#4665,10.);
#1376=VECTOR('',#4666,10.);
#1377=VECTOR('',#4679,10.);
#1378=VECTOR('',#4704,10.);
#1379=VECTOR('',#4709,10.);
#1380=VECTOR('',#4710,10.);
#1381=VECTOR('',#4731,10.);
#1382=VECTOR('',#4734,10.);
#1383=VECTOR('',#4737,10.);
#1384=VECTOR('',#4738,10.);
#1385=VECTOR('',#4765,10.);
#1386=VECTOR('',#4766,10.);
#1387=VECTOR('',#4769,10.);
#1388=VECTOR('',#4772,10.);
#1389=VECTOR('',#4775,10.);
#1390=VECTOR('',#4786,10.);
#1391=VECTOR('',#4789,10.);
#1392=VECTOR('',#4802,10.);
#1393=VECTOR('',#4803,10.);
#1394=VECTOR('',#4832,10.);
#1395=VECTOR('',#4833,10.);
#1396=VECTOR('',#4838,10.);
#1397=VECTOR('',#4849,10.);
#1398=VECTOR('',#4852,10.);
#1399=VECTOR('',#4853,10.);
#1400=VECTOR('',#4854,10.);
#1401=VECTOR('',#4855,10.);
#1402=VECTOR('',#4856,10.);
#1403=VECTOR('',#4859,10.);
#1404=VECTOR('',#4864,10.);
#1405=VECTOR('',#4865,10.);
#1406=VECTOR('',#4868,10.);
#1407=VECTOR('',#4873,10.);
#1408=VECTOR('',#4878,10.);
#1409=VECTOR('',#4883,10.);
#1410=VECTOR('',#4884,10.);
#1411=VECTOR('',#4891,10.);
#1412=VECTOR('',#4900,9.5);
#1413=VECTOR('',#4903,10.);
#1414=VECTOR('',#4904,10.);
#1415=VECTOR('',#4911,10.);
#1416=VECTOR('',#4920,4.);
#1417=VECTOR('',#4929,4.);
#1418=VECTOR('',#4932,3.99999999999999);
#1419=VECTOR('',#4937,3.99999999999999);
#1420=VECTOR('',#4940,10.);
#1421=VECTOR('',#4945,1.5);
#1422=VECTOR('',#4948,3.);
#1423=VECTOR('',#4953,1.5);
#1424=VECTOR('',#4956,3.);
#1425=VECTOR('',#4961,10.);
#1426=VECTOR('',#4966,10.);
#1606=VERTEX_POINT('',#5609);
#1607=VERTEX_POINT('',#5610);
#1608=VERTEX_POINT('',#5612);
#1609=VERTEX_POINT('',#5614);
#1610=VERTEX_POINT('',#5618);
#1611=VERTEX_POINT('',#5620);
#1612=VERTEX_POINT('',#5624);
#1613=VERTEX_POINT('',#5625);
#1614=VERTEX_POINT('',#5627);
#1615=VERTEX_POINT('',#5629);
#1616=VERTEX_POINT('',#5633);
#1617=VERTEX_POINT('',#5634);
#1618=VERTEX_POINT('',#5636);
#1619=VERTEX_POINT('',#5638);
#1620=VERTEX_POINT('',#5642);
#1621=VERTEX_POINT('',#5644);
#1622=VERTEX_POINT('',#5646);
#1623=VERTEX_POINT('',#5648);
#1624=VERTEX_POINT('',#5653);
#1625=VERTEX_POINT('',#5655);
#1626=VERTEX_POINT('',#5659);
#1627=VERTEX_POINT('',#5662);
#1628=VERTEX_POINT('',#5664);
#1629=VERTEX_POINT('',#5666);
#1630=VERTEX_POINT('',#5673);
#1631=VERTEX_POINT('',#5675);
#1632=VERTEX_POINT('',#5677);
#1633=VERTEX_POINT('',#5679);
#1634=VERTEX_POINT('',#5682);
#1635=VERTEX_POINT('',#5684);
#1636=VERTEX_POINT('',#5687);
#1637=VERTEX_POINT('',#5691);
#1638=VERTEX_POINT('',#5693);
#1639=VERTEX_POINT('',#5695);
#1640=VERTEX_POINT('',#5697);
#1641=VERTEX_POINT('',#5699);
#1642=VERTEX_POINT('',#5701);
#1643=VERTEX_POINT('',#5703);
#1644=VERTEX_POINT('',#5705);
#1645=VERTEX_POINT('',#5709);
#1646=VERTEX_POINT('',#5711);
#1647=VERTEX_POINT('',#5713);
#1648=VERTEX_POINT('',#5715);
#1649=VERTEX_POINT('',#5717);
#1650=VERTEX_POINT('',#5720);
#1651=VERTEX_POINT('',#5722);
#1652=VERTEX_POINT('',#5744);
#1653=VERTEX_POINT('',#5745);
#1654=VERTEX_POINT('',#5751);
#1655=VERTEX_POINT('',#5758);
#1656=VERTEX_POINT('',#5759);
#1657=VERTEX_POINT('',#5783);
#1658=VERTEX_POINT('',#5788);
#1659=VERTEX_POINT('',#5829);
#1660=VERTEX_POINT('',#5833);
#1661=VERTEX_POINT('',#5834);
#1662=VERTEX_POINT('',#5849);
#1663=VERTEX_POINT('',#5854);
#1664=VERTEX_POINT('',#5860);
#1665=VERTEX_POINT('',#5862);
#1666=VERTEX_POINT('',#5867);
#1667=VERTEX_POINT('',#5873);
#1668=VERTEX_POINT('',#5875);
#1669=VERTEX_POINT('',#5877);
#1670=VERTEX_POINT('',#5879);
#1671=VERTEX_POINT('',#5881);
#1672=VERTEX_POINT('',#5885);
#1673=VERTEX_POINT('',#5886);
#1674=VERTEX_POINT('',#5902);
#1675=VERTEX_POINT('',#5906);
#1676=VERTEX_POINT('',#5929);
#1677=VERTEX_POINT('',#5930);
#1678=VERTEX_POINT('',#5932);
#1679=VERTEX_POINT('',#5943);
#1680=VERTEX_POINT('',#5944);
#1681=VERTEX_POINT('',#5968);
#1682=VERTEX_POINT('',#5969);
#1683=VERTEX_POINT('',#6009);
#1684=VERTEX_POINT('',#6016);
#1685=VERTEX_POINT('',#6052);
#1686=VERTEX_POINT('',#6053);
#1687=VERTEX_POINT('',#6077);
#1688=VERTEX_POINT('',#6082);
#1689=VERTEX_POINT('',#6089);
#1690=VERTEX_POINT('',#6090);
#1691=VERTEX_POINT('',#6119);
#1692=VERTEX_POINT('',#6120);
#1693=VERTEX_POINT('',#6132);
#1694=VERTEX_POINT('',#6137);
#1695=VERTEX_POINT('',#6151);
#1696=VERTEX_POINT('',#6153);
#1697=VERTEX_POINT('',#6157);
#1698=VERTEX_POINT('',#6159);
#1699=VERTEX_POINT('',#6200);
#1700=VERTEX_POINT('',#6204);
#1701=VERTEX_POINT('',#6205);
#1702=VERTEX_POINT('',#6207);
#1703=VERTEX_POINT('',#6209);
#1704=VERTEX_POINT('',#6232);
#1705=VERTEX_POINT('',#6237);
#1706=VERTEX_POINT('',#6278);
#1707=VERTEX_POINT('',#6301);
#1708=VERTEX_POINT('',#6302);
#1709=VERTEX_POINT('',#6320);
#1710=VERTEX_POINT('',#6325);
#1711=VERTEX_POINT('',#6343);
#1712=VERTEX_POINT('',#6347);
#1713=VERTEX_POINT('',#6356);
#1714=VERTEX_POINT('',#6383);
#1715=VERTEX_POINT('',#6390);
#1716=VERTEX_POINT('',#6394);
#1717=VERTEX_POINT('',#6396);
#1718=VERTEX_POINT('',#6400);
#1719=VERTEX_POINT('',#6401);
#1720=VERTEX_POINT('',#6403);
#1721=VERTEX_POINT('',#6405);
#1722=VERTEX_POINT('',#6420);
#1723=VERTEX_POINT('',#6421);
#1724=VERTEX_POINT('',#6445);
#1725=VERTEX_POINT('',#6447);
#1726=VERTEX_POINT('',#6449);
#1727=VERTEX_POINT('',#6508);
#1728=VERTEX_POINT('',#6509);
#1729=VERTEX_POINT('',#6533);
#1730=VERTEX_POINT('',#6535);
#1731=VERTEX_POINT('',#6537);
#1732=VERTEX_POINT('',#6601);
#1733=VERTEX_POINT('',#6603);
#1734=VERTEX_POINT('',#6607);
#1735=VERTEX_POINT('',#6622);
#1736=VERTEX_POINT('',#6624);
#1737=VERTEX_POINT('',#6629);
#1738=VERTEX_POINT('',#6633);
#1739=VERTEX_POINT('',#6637);
#1740=VERTEX_POINT('',#6641);
#1741=VERTEX_POINT('',#6645);
#1742=VERTEX_POINT('',#6649);
#1743=VERTEX_POINT('',#6656);
#1744=VERTEX_POINT('',#6659);
#1745=VERTEX_POINT('',#6660);
#1746=VERTEX_POINT('',#6672);
#1747=VERTEX_POINT('',#6676);
#1748=VERTEX_POINT('',#6684);
#1749=VERTEX_POINT('',#6692);
#1750=VERTEX_POINT('',#6694);
#1751=VERTEX_POINT('',#6699);
#1752=VERTEX_POINT('',#6701);
#1964=EDGE_CURVE('',#1606,#1607,#1028,.T.);
#1965=EDGE_CURVE('',#1608,#1606,#1029,.T.);
#1966=EDGE_CURVE('',#1609,#1608,#1030,.T.);
#1967=EDGE_CURVE('',#1609,#1607,#1031,.T.);
#1968=EDGE_CURVE('',#1607,#1610,#1032,.T.);
#1969=EDGE_CURVE('',#1611,#1609,#1033,.T.);
#1970=EDGE_CURVE('',#1610,#1611,#1034,.T.);
#1971=EDGE_CURVE('',#1612,#1613,#1035,.T.);
#1972=EDGE_CURVE('',#1614,#1612,#1036,.T.);
#1973=EDGE_CURVE('',#1614,#1615,#1037,.T.);
#1974=EDGE_CURVE('',#1613,#1615,#1038,.T.);
#1975=EDGE_CURVE('',#1616,#1617,#1039,.T.);
#1976=EDGE_CURVE('',#1618,#1616,#1040,.T.);
#1977=EDGE_CURVE('',#1619,#1618,#1041,.T.);
#1978=EDGE_CURVE('',#1619,#1617,#1042,.T.);
#1979=EDGE_CURVE('',#1620,#1606,#1043,.T.);
#1980=EDGE_CURVE('',#1621,#1620,#1044,.T.);
#1981=EDGE_CURVE('',#1622,#1621,#1045,.T.);
#1982=EDGE_CURVE('',#1623,#1622,#1046,.T.);
#1983=EDGE_CURVE('',#1617,#1623,#1047,.T.);
#1984=EDGE_CURVE('',#1608,#1619,#1048,.T.);
#1985=EDGE_CURVE('',#1615,#1624,#1049,.T.);
#1986=EDGE_CURVE('',#1625,#1614,#1050,.T.);
#1987=EDGE_CURVE('',#1625,#1624,#1051,.T.);
#1988=EDGE_CURVE('',#1624,#1626,#1052,.T.);
#1989=EDGE_CURVE('',#1618,#1625,#1053,.T.);
#1990=EDGE_CURVE('',#1627,#1616,#1054,.T.);
#1991=EDGE_CURVE('',#1628,#1627,#1055,.T.);
#1992=EDGE_CURVE('',#1629,#1628,#1056,.T.);
#1993=EDGE_CURVE('',#1629,#1626,#1057,.T.);
#1994=EDGE_CURVE('',#1626,#1620,#1058,.T.);
#1995=EDGE_CURVE('',#1621,#1629,#1059,.T.);
#1996=EDGE_CURVE('',#1628,#1630,#1060,.T.);
#1997=EDGE_CURVE('',#1631,#1630,#1061,.T.);
#1998=EDGE_CURVE('',#1632,#1631,#1062,.T.);
#1999=EDGE_CURVE('',#1633,#1632,#1063,.T.);
#2000=EDGE_CURVE('',#1633,#1622,#1064,.T.);
#2001=EDGE_CURVE('',#1634,#1634,#369,.T.);
#2002=EDGE_CURVE('',#1635,#1635,#370,.T.);
#2003=EDGE_CURVE('',#1627,#1636,#1065,.T.);
#2004=EDGE_CURVE('',#1630,#1636,#1066,.T.);
#2005=EDGE_CURVE('',#1637,#1610,#1067,.T.);
#2006=EDGE_CURVE('',#1638,#1637,#1068,.T.);
#2007=EDGE_CURVE('',#1639,#1638,#371,.T.);
#2008=EDGE_CURVE('',#1640,#1639,#1069,.T.);
#2009=EDGE_CURVE('',#1640,#1641,#1070,.T.);
#2010=EDGE_CURVE('',#1642,#1641,#1071,.T.);
#2011=EDGE_CURVE('',#1643,#1642,#372,.T.);
#2012=EDGE_CURVE('',#1644,#1643,#1072,.T.);
#2013=EDGE_CURVE('',#1613,#1644,#1073,.T.);
#2014=EDGE_CURVE('',#1645,#1611,#1074,.T.);
#2015=EDGE_CURVE('',#1646,#1645,#373,.T.);
#2016=EDGE_CURVE('',#1647,#1646,#374,.T.);
#2017=EDGE_CURVE('',#1648,#1647,#1075,.T.);
#2018=EDGE_CURVE('',#1649,#1648,#375,.T.);
#2019=EDGE_CURVE('',#1637,#1649,#376,.T.);
#2020=EDGE_CURVE('',#1650,#1650,#377,.T.);
#2021=EDGE_CURVE('',#1651,#1651,#378,.T.);
#2022=EDGE_CURVE('',#1652,#1653,#379,.T.);
#2023=EDGE_CURVE('',#1653,#1643,#207,.T.);
#2024=EDGE_CURVE('',#1643,#1654,#380,.T.);
#2025=EDGE_CURVE('',#1654,#1652,#208,.T.);
#2026=EDGE_CURVE('',#1655,#1656,#381,.T.);
#2027=EDGE_CURVE('',#1656,#1653,#382,.T.);
#2028=EDGE_CURVE('',#1652,#1655,#383,.T.);
#2029=EDGE_CURVE('',#1655,#1657,#209,.T.);
#2030=EDGE_CURVE('',#1657,#1658,#384,.T.);
#2031=EDGE_CURVE('',#1658,#1656,#210,.T.);
#2032=EDGE_CURVE('',#1657,#1659,#169,.T.);
#2033=EDGE_CURVE('',#1659,#1658,#170,.T.);
#2034=EDGE_CURVE('',#1660,#1661,#211,.T.);
#2035=EDGE_CURVE('',#1661,#1662,#385,.T.);
#2036=EDGE_CURVE('',#1662,#1641,#386,.T.);
#2037=EDGE_CURVE('',#1641,#1660,#387,.T.);
#2038=EDGE_CURVE('',#1663,#1642,#388,.T.);
#2039=EDGE_CURVE('',#1662,#1663,#1076,.T.);
#2040=EDGE_CURVE('',#1663,#1654,#389,.T.);
#2041=EDGE_CURVE('',#1659,#1664,#1077,.T.);
#2042=EDGE_CURVE('',#1664,#1665,#390,.T.);
#2043=EDGE_CURVE('',#1665,#1658,#1078,.T.);
#2044=EDGE_CURVE('',#1655,#1652,#1079,.T.);
#2045=EDGE_CURVE('',#1666,#1666,#391,.T.);
#2046=EDGE_CURVE('',#1663,#1659,#1080,.T.);
#2047=EDGE_CURVE('',#1661,#1631,#1081,.T.);
#2048=EDGE_CURVE('',#1636,#1667,#1082,.T.);
#2049=EDGE_CURVE('',#1668,#1667,#1083,.T.);
#2050=EDGE_CURVE('',#1669,#1668,#1084,.T.);
#2051=EDGE_CURVE('',#1670,#1669,#1085,.T.);
#2052=EDGE_CURVE('',#1671,#1670,#1086,.T.);
#2053=EDGE_CURVE('',#1671,#1664,#1087,.T.);
#2054=EDGE_CURVE('',#1672,#1673,#212,.T.);
#2055=EDGE_CURVE('',#1673,#1640,#392,.T.);
#2056=EDGE_CURVE('',#1640,#1674,#393,.T.);
#2057=EDGE_CURVE('',#1674,#1672,#394,.T.);
#2058=EDGE_CURVE('',#1639,#1675,#395,.T.);
#2059=EDGE_CURVE('',#1675,#1674,#1088,.T.);
#2060=EDGE_CURVE('',#1676,#1677,#396,.T.);
#2061=EDGE_CURVE('',#1677,#1678,#213,.T.);
#2062=EDGE_CURVE('',#1678,#1638,#397,.T.);
#2063=EDGE_CURVE('',#1638,#1676,#214,.T.);
#2064=EDGE_CURVE('',#1679,#1680,#398,.T.);
#2065=EDGE_CURVE('',#1680,#1677,#399,.T.);
#2066=EDGE_CURVE('',#1676,#1679,#400,.T.);
#2067=EDGE_CURVE('',#1681,#1682,#401,.T.);
#2068=EDGE_CURVE('',#1682,#1680,#215,.T.);
#2069=EDGE_CURVE('',#1679,#1681,#216,.T.);
#2070=EDGE_CURVE('',#1681,#1683,#171,.T.);
#2071=EDGE_CURVE('',#1683,#1682,#172,.T.);
#2072=EDGE_CURVE('',#1678,#1675,#402,.T.);
#2073=EDGE_CURVE('',#1677,#1680,#1089,.T.);
#2074=EDGE_CURVE('',#1684,#1684,#403,.T.);
#2075=EDGE_CURVE('',#1681,#1649,#1090,.T.);
#2076=EDGE_CURVE('',#1648,#1683,#1091,.T.);
#2077=EDGE_CURVE('',#1685,#1686,#404,.T.);
#2078=EDGE_CURVE('',#1686,#1670,#173,.T.);
#2079=EDGE_CURVE('',#1670,#1685,#174,.T.);
#2080=EDGE_CURVE('',#1685,#1687,#217,.T.);
#2081=EDGE_CURVE('',#1687,#1688,#405,.T.);
#2082=EDGE_CURVE('',#1688,#1686,#218,.T.);
#2083=EDGE_CURVE('',#1689,#1690,#406,.T.);
#2084=EDGE_CURVE('',#1690,#1688,#407,.T.);
#2085=EDGE_CURVE('',#1687,#1689,#408,.T.);
#2086=EDGE_CURVE('',#1691,#1692,#219,.T.);
#2087=EDGE_CURVE('',#1692,#1690,#220,.T.);
#2088=EDGE_CURVE('',#1689,#1693,#221,.T.);
#2089=EDGE_CURVE('',#1693,#1694,#222,.T.);
#2090=EDGE_CURVE('',#1694,#1691,#223,.T.);
#2091=EDGE_CURVE('',#1695,#1692,#1092,.T.);
#2092=EDGE_CURVE('',#1695,#1696,#409,.T.);
#2093=EDGE_CURVE('',#1686,#1696,#1093,.T.);
#2094=EDGE_CURVE('',#1697,#1691,#1094,.F.);
#2095=EDGE_CURVE('',#1697,#1698,#224,.T.);
#2096=EDGE_CURVE('',#1698,#1695,#1095,.T.);
#2097=EDGE_CURVE('',#1694,#1697,#225,.T.);
#2098=EDGE_CURVE('',#1693,#1669,#175,.T.);
#2099=EDGE_CURVE('',#1699,#1669,#410,.T.);
#2100=EDGE_CURVE('',#1699,#1698,#176,.T.);
#2101=EDGE_CURVE('',#1700,#1701,#411,.T.);
#2102=EDGE_CURVE('',#1701,#1702,#412,.T.);
#2103=EDGE_CURVE('',#1702,#1703,#413,.T.);
#2104=EDGE_CURVE('',#1703,#1700,#414,.T.);
#2105=EDGE_CURVE('',#1700,#1704,#226,.T.);
#2106=EDGE_CURVE('',#1704,#1705,#415,.T.);
#2107=EDGE_CURVE('',#1705,#1701,#227,.T.);
#2108=EDGE_CURVE('',#1704,#1706,#177,.T.);
#2109=EDGE_CURVE('',#1706,#1705,#178,.T.);
#2110=EDGE_CURVE('',#1707,#1708,#228,.T.);
#2111=EDGE_CURVE('',#1708,#1703,#229,.T.);
#2112=EDGE_CURVE('',#1702,#1709,#230,.T.);
#2113=EDGE_CURVE('',#1709,#1710,#231,.T.);
#2114=EDGE_CURVE('',#1710,#1707,#232,.T.);
#2115=EDGE_CURVE('',#1706,#1647,#1096,.T.);
#2116=EDGE_CURVE('',#1646,#1705,#1097,.T.);
#2117=EDGE_CURVE('',#1700,#1703,#1098,.T.);
#2118=EDGE_CURVE('',#1711,#1708,#179,.T.);
#2119=EDGE_CURVE('',#1711,#1706,#1099,.T.);
#2120=EDGE_CURVE('',#1710,#1712,#1100,.T.);
#2121=EDGE_CURVE('',#1707,#1712,#233,.F.);
#2122=EDGE_CURVE('',#1713,#1713,#416,.T.);
#2123=EDGE_CURVE('',#1712,#1714,#234,.F.);
#2124=EDGE_CURVE('',#1714,#1715,#180,.T.);
#2125=EDGE_CURVE('',#1711,#1715,#417,.T.);
#2126=EDGE_CURVE('',#1715,#1716,#1101,.T.);
#2127=EDGE_CURVE('',#1716,#1717,#418,.T.);
#2128=EDGE_CURVE('',#1717,#1711,#1102,.T.);
#2129=EDGE_CURVE('',#1718,#1719,#419,.T.);
#2130=EDGE_CURVE('',#1719,#1720,#420,.T.);
#2131=EDGE_CURVE('',#1720,#1721,#421,.T.);
#2132=EDGE_CURVE('',#1721,#1718,#235,.T.);
#2133=EDGE_CURVE('',#1722,#1723,#422,.T.);
#2134=EDGE_CURVE('',#1723,#1720,#1103,.T.);
#2135=EDGE_CURVE('',#1719,#1722,#1104,.T.);
#2136=EDGE_CURVE('',#1721,#1724,#181,.T.);
#2137=EDGE_CURVE('',#1724,#1725,#423,.T.);
#2138=EDGE_CURVE('',#1725,#1726,#182,.T.);
#2139=EDGE_CURVE('',#1726,#1718,#236,.T.);
#2140=EDGE_CURVE('',#1727,#1728,#424,.T.);
#2141=EDGE_CURVE('',#1728,#1725,#183,.T.);
#2142=EDGE_CURVE('',#1724,#1727,#184,.T.);
#2143=EDGE_CURVE('',#1729,#1728,#185,.T.);
#2144=EDGE_CURVE('',#1727,#1730,#186,.T.);
#2145=EDGE_CURVE('',#1730,#1731,#237,.T.);
#2146=EDGE_CURVE('',#1731,#1729,#238,.T.);
#2147=EDGE_CURVE('',#1730,#1732,#425,.T.);
#2148=EDGE_CURVE('',#1732,#1733,#426,.T.);
#2149=EDGE_CURVE('',#1733,#1731,#427,.T.);
#2150=EDGE_CURVE('',#1734,#1716,#428,.T.);
#2151=EDGE_CURVE('',#1716,#1733,#1105,.T.);
#2152=EDGE_CURVE('',#1732,#1734,#1106,.T.);
#2153=EDGE_CURVE('',#1668,#1722,#429,.T.);
#2154=EDGE_CURVE('',#1722,#1699,#1107,.T.);
#2155=EDGE_CURVE('',#1668,#1723,#430,.T.);
#2156=EDGE_CURVE('',#1734,#1717,#431,.T.);
#2157=EDGE_CURVE('',#1645,#1709,#1108,.T.);
#2158=EDGE_CURVE('',#1683,#1675,#1109,.T.);
#2159=EDGE_CURVE('',#1735,#1717,#1110,.T.);
#2160=EDGE_CURVE('',#1735,#1736,#1111,.T.);
#2161=EDGE_CURVE('',#1736,#1633,#1112,.T.);
#2162=EDGE_CURVE('',#1632,#1672,#1113,.T.);
#2163=EDGE_CURVE('',#1734,#1737,#1114,.T.);
#2164=EDGE_CURVE('',#1737,#1735,#187,.T.);
#2165=EDGE_CURVE('',#1738,#1732,#1115,.T.);
#2166=EDGE_CURVE('',#1737,#1738,#1116,.T.);
#2167=EDGE_CURVE('',#1739,#1727,#1117,.T.);
#2168=EDGE_CURVE('',#1738,#1739,#188,.T.);
#2169=EDGE_CURVE('',#1740,#1724,#1118,.T.);
#2170=EDGE_CURVE('',#1739,#1740,#189,.T.);
#2171=EDGE_CURVE('',#1741,#1720,#1119,.T.);
#2172=EDGE_CURVE('',#1740,#1741,#190,.T.);
#2173=EDGE_CURVE('',#1742,#1723,#1120,.T.);
#2174=EDGE_CURVE('',#1741,#1742,#1121,.T.);
#2175=EDGE_CURVE('',#1667,#1742,#191,.T.);
#2176=EDGE_CURVE('',#1736,#1623,#1122,.T.);
#2177=EDGE_CURVE('',#1743,#1743,#432,.T.);
#2178=EDGE_CURVE('',#1744,#1745,#192,.T.);
#2179=EDGE_CURVE('',#1745,#1744,#433,.T.);
#2180=EDGE_CURVE('',#1745,#1743,#1123,.T.);
#2181=EDGE_CURVE('',#1729,#1745,#1124,.T.);
#2182=EDGE_CURVE('',#1744,#1726,#1125,.T.);
#2183=EDGE_CURVE('',#1696,#1671,#434,.T.);
#2184=EDGE_CURVE('',#1689,#1687,#1126,.T.);
#2185=EDGE_CURVE('',#1746,#1746,#435,.T.);
#2186=EDGE_CURVE('',#1666,#1747,#1127,.T.);
#2187=EDGE_CURVE('',#1747,#1747,#436,.T.);
#2188=EDGE_CURVE('',#1665,#1644,#437,.T.);
#2189=EDGE_CURVE('',#1684,#1650,#1128,.T.);
#2190=EDGE_CURVE('',#1746,#1748,#1129,.T.);
#2191=EDGE_CURVE('',#1748,#1748,#438,.T.);
#2192=EDGE_CURVE('',#1713,#1651,#1130,.T.);
#2193=EDGE_CURVE('',#1645,#1714,#1131,.T.);
#2194=EDGE_CURVE('',#1749,#1749,#439,.T.);
#2195=EDGE_CURVE('',#1749,#1750,#1132,.T.);
#2196=EDGE_CURVE('',#1635,#1749,#1133,.T.);
#2197=EDGE_CURVE('',#1751,#1751,#440,.T.);
#2198=EDGE_CURVE('',#1751,#1752,#1134,.T.);
#2199=EDGE_CURVE('',#1634,#1751,#1135,.T.);
#2200=EDGE_CURVE('',#1673,#1660,#1136,.T.);
#2201=EDGE_CURVE('',#1612,#1695,#1137,.T.);
#2527=ORIENTED_EDGE('',*,*,#1964,.F.);
#2528=ORIENTED_EDGE('',*,*,#1965,.F.);
#2529=ORIENTED_EDGE('',*,*,#1966,.F.);
#2530=ORIENTED_EDGE('',*,*,#1967,.T.);
#2531=ORIENTED_EDGE('',*,*,#1968,.F.);
#2532=ORIENTED_EDGE('',*,*,#1967,.F.);
#2533=ORIENTED_EDGE('',*,*,#1969,.F.);
#2534=ORIENTED_EDGE('',*,*,#1970,.F.);
#2535=ORIENTED_EDGE('',*,*,#1971,.F.);
#2536=ORIENTED_EDGE('',*,*,#1972,.F.);
#2537=ORIENTED_EDGE('',*,*,#1973,.T.);
#2538=ORIENTED_EDGE('',*,*,#1974,.F.);
#2539=ORIENTED_EDGE('',*,*,#1975,.F.);
#2540=ORIENTED_EDGE('',*,*,#1976,.F.);
#2541=ORIENTED_EDGE('',*,*,#1977,.F.);
#2542=ORIENTED_EDGE('',*,*,#1978,.T.);
#2543=ORIENTED_EDGE('',*,*,#1979,.F.);
#2544=ORIENTED_EDGE('',*,*,#1980,.F.);
#2545=ORIENTED_EDGE('',*,*,#1981,.F.);
#2546=ORIENTED_EDGE('',*,*,#1982,.F.);
#2547=ORIENTED_EDGE('',*,*,#1983,.F.);
#2548=ORIENTED_EDGE('',*,*,#1978,.F.);
#2549=ORIENTED_EDGE('',*,*,#1984,.F.);
#2550=ORIENTED_EDGE('',*,*,#1965,.T.);
#2551=ORIENTED_EDGE('',*,*,#1985,.F.);
#2552=ORIENTED_EDGE('',*,*,#1973,.F.);
#2553=ORIENTED_EDGE('',*,*,#1986,.F.);
#2554=ORIENTED_EDGE('',*,*,#1987,.T.);
#2555=ORIENTED_EDGE('',*,*,#1988,.F.);
#2556=ORIENTED_EDGE('',*,*,#1987,.F.);
#2557=ORIENTED_EDGE('',*,*,#1989,.F.);
#2558=ORIENTED_EDGE('',*,*,#1976,.T.);
#2559=ORIENTED_EDGE('',*,*,#1990,.F.);
#2560=ORIENTED_EDGE('',*,*,#1991,.F.);
#2561=ORIENTED_EDGE('',*,*,#1992,.F.);
#2562=ORIENTED_EDGE('',*,*,#1993,.T.);
#2563=ORIENTED_EDGE('',*,*,#1994,.F.);
#2564=ORIENTED_EDGE('',*,*,#1993,.F.);
#2565=ORIENTED_EDGE('',*,*,#1995,.F.);
#2566=ORIENTED_EDGE('',*,*,#1980,.T.);
#2567=ORIENTED_EDGE('',*,*,#1981,.T.);
#2568=ORIENTED_EDGE('',*,*,#1995,.T.);
#2569=ORIENTED_EDGE('',*,*,#1992,.T.);
#2570=ORIENTED_EDGE('',*,*,#1996,.T.);
#2571=ORIENTED_EDGE('',*,*,#1997,.F.);
#2572=ORIENTED_EDGE('',*,*,#1998,.F.);
#2573=ORIENTED_EDGE('',*,*,#1999,.F.);
#2574=ORIENTED_EDGE('',*,*,#2000,.T.);
#2575=ORIENTED_EDGE('',*,*,#2001,.T.);
#2576=ORIENTED_EDGE('',*,*,#2002,.T.);
#2577=ORIENTED_EDGE('',*,*,#1991,.T.);
#2578=ORIENTED_EDGE('',*,*,#2003,.T.);
#2579=ORIENTED_EDGE('',*,*,#2004,.F.);
#2580=ORIENTED_EDGE('',*,*,#1996,.F.);
#2581=ORIENTED_EDGE('',*,*,#1974,.T.);
#2582=ORIENTED_EDGE('',*,*,#1985,.T.);
#2583=ORIENTED_EDGE('',*,*,#1988,.T.);
#2584=ORIENTED_EDGE('',*,*,#1994,.T.);
#2585=ORIENTED_EDGE('',*,*,#1979,.T.);
#2586=ORIENTED_EDGE('',*,*,#1964,.T.);
#2587=ORIENTED_EDGE('',*,*,#1968,.T.);
#2588=ORIENTED_EDGE('',*,*,#2005,.F.);
#2589=ORIENTED_EDGE('',*,*,#2006,.F.);
#2590=ORIENTED_EDGE('',*,*,#2007,.F.);
#2591=ORIENTED_EDGE('',*,*,#2008,.F.);
#2592=ORIENTED_EDGE('',*,*,#2009,.T.);
#2593=ORIENTED_EDGE('',*,*,#2010,.F.);
#2594=ORIENTED_EDGE('',*,*,#2011,.F.);
#2595=ORIENTED_EDGE('',*,*,#2012,.F.);
#2596=ORIENTED_EDGE('',*,*,#2013,.F.);
#2597=ORIENTED_EDGE('',*,*,#1970,.T.);
#2598=ORIENTED_EDGE('',*,*,#2014,.F.);
#2599=ORIENTED_EDGE('',*,*,#2015,.F.);
#2600=ORIENTED_EDGE('',*,*,#2016,.F.);
#2601=ORIENTED_EDGE('',*,*,#2017,.F.);
#2602=ORIENTED_EDGE('',*,*,#2018,.F.);
#2603=ORIENTED_EDGE('',*,*,#2019,.F.);
#2604=ORIENTED_EDGE('',*,*,#2005,.T.);
#2605=ORIENTED_EDGE('',*,*,#2020,.F.);
#2606=ORIENTED_EDGE('',*,*,#2021,.F.);
#2607=ORIENTED_EDGE('',*,*,#2022,.T.);
#2608=ORIENTED_EDGE('',*,*,#2023,.T.);
#2609=ORIENTED_EDGE('',*,*,#2024,.T.);
#2610=ORIENTED_EDGE('',*,*,#2025,.T.);
#2611=ORIENTED_EDGE('',*,*,#2026,.T.);
#2612=ORIENTED_EDGE('',*,*,#2027,.T.);
#2613=ORIENTED_EDGE('',*,*,#2022,.F.);
#2614=ORIENTED_EDGE('',*,*,#2028,.T.);
#2615=ORIENTED_EDGE('',*,*,#2026,.F.);
#2616=ORIENTED_EDGE('',*,*,#2029,.T.);
#2617=ORIENTED_EDGE('',*,*,#2030,.T.);
#2618=ORIENTED_EDGE('',*,*,#2031,.T.);
#2619=ORIENTED_EDGE('',*,*,#2032,.T.);
#2620=ORIENTED_EDGE('',*,*,#2033,.T.);
#2621=ORIENTED_EDGE('',*,*,#2030,.F.);
#2622=ORIENTED_EDGE('',*,*,#2034,.T.);
#2623=ORIENTED_EDGE('',*,*,#2035,.T.);
#2624=ORIENTED_EDGE('',*,*,#2036,.T.);
#2625=ORIENTED_EDGE('',*,*,#2037,.T.);
#2626=ORIENTED_EDGE('',*,*,#2038,.T.);
#2627=ORIENTED_EDGE('',*,*,#2010,.T.);
#2628=ORIENTED_EDGE('',*,*,#2036,.F.);
#2629=ORIENTED_EDGE('',*,*,#2039,.T.);
#2630=ORIENTED_EDGE('',*,*,#2038,.F.);
#2631=ORIENTED_EDGE('',*,*,#2040,.T.);
#2632=ORIENTED_EDGE('',*,*,#2024,.F.);
#2633=ORIENTED_EDGE('',*,*,#2011,.T.);
#2634=ORIENTED_EDGE('',*,*,#2033,.F.);
#2635=ORIENTED_EDGE('',*,*,#2041,.T.);
#2636=ORIENTED_EDGE('',*,*,#2042,.T.);
#2637=ORIENTED_EDGE('',*,*,#2043,.T.);
#2638=ORIENTED_EDGE('',*,*,#2028,.F.);
#2639=ORIENTED_EDGE('',*,*,#2044,.F.);
#2640=ORIENTED_EDGE('',*,*,#2045,.T.);
#2641=ORIENTED_EDGE('',*,*,#2032,.F.);
#2642=ORIENTED_EDGE('',*,*,#2029,.F.);
#2643=ORIENTED_EDGE('',*,*,#2044,.T.);
#2644=ORIENTED_EDGE('',*,*,#2025,.F.);
#2645=ORIENTED_EDGE('',*,*,#2040,.F.);
#2646=ORIENTED_EDGE('',*,*,#2046,.T.);
#2647=ORIENTED_EDGE('',*,*,#2039,.F.);
#2648=ORIENTED_EDGE('',*,*,#2035,.F.);
#2649=ORIENTED_EDGE('',*,*,#2047,.T.);
#2650=ORIENTED_EDGE('',*,*,#1997,.T.);
#2651=ORIENTED_EDGE('',*,*,#2004,.T.);
#2652=ORIENTED_EDGE('',*,*,#2048,.T.);
#2653=ORIENTED_EDGE('',*,*,#2049,.F.);
#2654=ORIENTED_EDGE('',*,*,#2050,.F.);
#2655=ORIENTED_EDGE('',*,*,#2051,.F.);
#2656=ORIENTED_EDGE('',*,*,#2052,.F.);
#2657=ORIENTED_EDGE('',*,*,#2053,.T.);
#2658=ORIENTED_EDGE('',*,*,#2041,.F.);
#2659=ORIENTED_EDGE('',*,*,#2046,.F.);
#2660=ORIENTED_EDGE('',*,*,#2054,.T.);
#2661=ORIENTED_EDGE('',*,*,#2055,.T.);
#2662=ORIENTED_EDGE('',*,*,#2056,.T.);
#2663=ORIENTED_EDGE('',*,*,#2057,.T.);
#2664=ORIENTED_EDGE('',*,*,#2058,.T.);
#2665=ORIENTED_EDGE('',*,*,#2059,.T.);
#2666=ORIENTED_EDGE('',*,*,#2056,.F.);
#2667=ORIENTED_EDGE('',*,*,#2008,.T.);
#2668=ORIENTED_EDGE('',*,*,#2060,.T.);
#2669=ORIENTED_EDGE('',*,*,#2061,.T.);
#2670=ORIENTED_EDGE('',*,*,#2062,.T.);
#2671=ORIENTED_EDGE('',*,*,#2063,.T.);
#2672=ORIENTED_EDGE('',*,*,#2064,.T.);
#2673=ORIENTED_EDGE('',*,*,#2065,.T.);
#2674=ORIENTED_EDGE('',*,*,#2060,.F.);
#2675=ORIENTED_EDGE('',*,*,#2066,.T.);
#2676=ORIENTED_EDGE('',*,*,#2067,.T.);
#2677=ORIENTED_EDGE('',*,*,#2068,.T.);
#2678=ORIENTED_EDGE('',*,*,#2064,.F.);
#2679=ORIENTED_EDGE('',*,*,#2069,.T.);
#2680=ORIENTED_EDGE('',*,*,#2067,.F.);
#2681=ORIENTED_EDGE('',*,*,#2070,.T.);
#2682=ORIENTED_EDGE('',*,*,#2071,.T.);
#2683=ORIENTED_EDGE('',*,*,#2062,.F.);
#2684=ORIENTED_EDGE('',*,*,#2072,.T.);
#2685=ORIENTED_EDGE('',*,*,#2058,.F.);
#2686=ORIENTED_EDGE('',*,*,#2007,.T.);
#2687=ORIENTED_EDGE('',*,*,#2065,.F.);
#2688=ORIENTED_EDGE('',*,*,#2073,.F.);
#2689=ORIENTED_EDGE('',*,*,#2074,.T.);
#2690=ORIENTED_EDGE('',*,*,#2070,.F.);
#2691=ORIENTED_EDGE('',*,*,#2075,.T.);
#2692=ORIENTED_EDGE('',*,*,#2018,.T.);
#2693=ORIENTED_EDGE('',*,*,#2076,.T.);
#2694=ORIENTED_EDGE('',*,*,#2069,.F.);
#2695=ORIENTED_EDGE('',*,*,#2066,.F.);
#2696=ORIENTED_EDGE('',*,*,#2063,.F.);
#2697=ORIENTED_EDGE('',*,*,#2006,.T.);
#2698=ORIENTED_EDGE('',*,*,#2019,.T.);
#2699=ORIENTED_EDGE('',*,*,#2075,.F.);
#2700=ORIENTED_EDGE('',*,*,#2077,.T.);
#2701=ORIENTED_EDGE('',*,*,#2078,.T.);
#2702=ORIENTED_EDGE('',*,*,#2079,.T.);
#2703=ORIENTED_EDGE('',*,*,#2077,.F.);
#2704=ORIENTED_EDGE('',*,*,#2080,.T.);
#2705=ORIENTED_EDGE('',*,*,#2081,.T.);
#2706=ORIENTED_EDGE('',*,*,#2082,.T.);
#2707=ORIENTED_EDGE('',*,*,#2083,.T.);
#2708=ORIENTED_EDGE('',*,*,#2084,.T.);
#2709=ORIENTED_EDGE('',*,*,#2081,.F.);
#2710=ORIENTED_EDGE('',*,*,#2085,.T.);
#2711=ORIENTED_EDGE('',*,*,#2086,.T.);
#2712=ORIENTED_EDGE('',*,*,#2087,.T.);
#2713=ORIENTED_EDGE('',*,*,#2083,.F.);
#2714=ORIENTED_EDGE('',*,*,#2088,.T.);
#2715=ORIENTED_EDGE('',*,*,#2089,.T.);
#2716=ORIENTED_EDGE('',*,*,#2090,.T.);
#2717=ORIENTED_EDGE('',*,*,#2082,.F.);
#2718=ORIENTED_EDGE('',*,*,#2084,.F.);
#2719=ORIENTED_EDGE('',*,*,#2087,.F.);
#2720=ORIENTED_EDGE('',*,*,#2091,.F.);
#2721=ORIENTED_EDGE('',*,*,#2092,.T.);
#2722=ORIENTED_EDGE('',*,*,#2093,.F.);
#2723=ORIENTED_EDGE('',*,*,#2086,.F.);
#2724=ORIENTED_EDGE('',*,*,#2094,.F.);
#2725=ORIENTED_EDGE('',*,*,#2095,.T.);
#2726=ORIENTED_EDGE('',*,*,#2096,.T.);
#2727=ORIENTED_EDGE('',*,*,#2091,.T.);
#2728=ORIENTED_EDGE('',*,*,#2090,.F.);
#2729=ORIENTED_EDGE('',*,*,#2097,.T.);
#2730=ORIENTED_EDGE('',*,*,#2094,.T.);
#2731=ORIENTED_EDGE('',*,*,#2089,.F.);
#2732=ORIENTED_EDGE('',*,*,#2098,.T.);
#2733=ORIENTED_EDGE('',*,*,#2099,.F.);
#2734=ORIENTED_EDGE('',*,*,#2100,.T.);
#2735=ORIENTED_EDGE('',*,*,#2095,.F.);
#2736=ORIENTED_EDGE('',*,*,#2097,.F.);
#2737=ORIENTED_EDGE('',*,*,#2101,.T.);
#2738=ORIENTED_EDGE('',*,*,#2102,.T.);
#2739=ORIENTED_EDGE('',*,*,#2103,.T.);
#2740=ORIENTED_EDGE('',*,*,#2104,.T.);
#2741=ORIENTED_EDGE('',*,*,#2101,.F.);
#2742=ORIENTED_EDGE('',*,*,#2105,.T.);
#2743=ORIENTED_EDGE('',*,*,#2106,.T.);
#2744=ORIENTED_EDGE('',*,*,#2107,.T.);
#2745=ORIENTED_EDGE('',*,*,#2108,.T.);
#2746=ORIENTED_EDGE('',*,*,#2109,.T.);
#2747=ORIENTED_EDGE('',*,*,#2106,.F.);
#2748=ORIENTED_EDGE('',*,*,#2110,.T.);
#2749=ORIENTED_EDGE('',*,*,#2111,.T.);
#2750=ORIENTED_EDGE('',*,*,#2103,.F.);
#2751=ORIENTED_EDGE('',*,*,#2112,.T.);
#2752=ORIENTED_EDGE('',*,*,#2113,.T.);
#2753=ORIENTED_EDGE('',*,*,#2114,.T.);
#2754=ORIENTED_EDGE('',*,*,#2109,.F.);
#2755=ORIENTED_EDGE('',*,*,#2115,.T.);
#2756=ORIENTED_EDGE('',*,*,#2016,.T.);
#2757=ORIENTED_EDGE('',*,*,#2116,.T.);
#2758=ORIENTED_EDGE('',*,*,#2108,.F.);
#2759=ORIENTED_EDGE('',*,*,#2105,.F.);
#2760=ORIENTED_EDGE('',*,*,#2117,.T.);
#2761=ORIENTED_EDGE('',*,*,#2111,.F.);
#2762=ORIENTED_EDGE('',*,*,#2118,.F.);
#2763=ORIENTED_EDGE('',*,*,#2119,.T.);
#2764=ORIENTED_EDGE('',*,*,#2114,.F.);
#2765=ORIENTED_EDGE('',*,*,#2120,.T.);
#2766=ORIENTED_EDGE('',*,*,#2121,.F.);
#2767=ORIENTED_EDGE('',*,*,#2104,.F.);
#2768=ORIENTED_EDGE('',*,*,#2117,.F.);
#2769=ORIENTED_EDGE('',*,*,#2122,.T.);
#2770=ORIENTED_EDGE('',*,*,#2110,.F.);
#2771=ORIENTED_EDGE('',*,*,#2121,.T.);
#2772=ORIENTED_EDGE('',*,*,#2123,.T.);
#2773=ORIENTED_EDGE('',*,*,#2124,.T.);
#2774=ORIENTED_EDGE('',*,*,#2125,.F.);
#2775=ORIENTED_EDGE('',*,*,#2118,.T.);
#2776=ORIENTED_EDGE('',*,*,#2125,.T.);
#2777=ORIENTED_EDGE('',*,*,#2126,.T.);
#2778=ORIENTED_EDGE('',*,*,#2127,.T.);
#2779=ORIENTED_EDGE('',*,*,#2128,.T.);
#2780=ORIENTED_EDGE('',*,*,#2129,.T.);
#2781=ORIENTED_EDGE('',*,*,#2130,.T.);
#2782=ORIENTED_EDGE('',*,*,#2131,.T.);
#2783=ORIENTED_EDGE('',*,*,#2132,.T.);
#2784=ORIENTED_EDGE('',*,*,#2133,.T.);
#2785=ORIENTED_EDGE('',*,*,#2134,.T.);
#2786=ORIENTED_EDGE('',*,*,#2130,.F.);
#2787=ORIENTED_EDGE('',*,*,#2135,.T.);
#2788=ORIENTED_EDGE('',*,*,#2136,.T.);
#2789=ORIENTED_EDGE('',*,*,#2137,.T.);
#2790=ORIENTED_EDGE('',*,*,#2138,.T.);
#2791=ORIENTED_EDGE('',*,*,#2139,.T.);
#2792=ORIENTED_EDGE('',*,*,#2132,.F.);
#2793=ORIENTED_EDGE('',*,*,#2140,.T.);
#2794=ORIENTED_EDGE('',*,*,#2141,.T.);
#2795=ORIENTED_EDGE('',*,*,#2137,.F.);
#2796=ORIENTED_EDGE('',*,*,#2142,.T.);
#2797=ORIENTED_EDGE('',*,*,#2143,.T.);
#2798=ORIENTED_EDGE('',*,*,#2140,.F.);
#2799=ORIENTED_EDGE('',*,*,#2144,.T.);
#2800=ORIENTED_EDGE('',*,*,#2145,.T.);
#2801=ORIENTED_EDGE('',*,*,#2146,.T.);
#2802=ORIENTED_EDGE('',*,*,#2147,.T.);
#2803=ORIENTED_EDGE('',*,*,#2148,.T.);
#2804=ORIENTED_EDGE('',*,*,#2149,.T.);
#2805=ORIENTED_EDGE('',*,*,#2145,.F.);
#2806=ORIENTED_EDGE('',*,*,#2150,.T.);
#2807=ORIENTED_EDGE('',*,*,#2151,.T.);
#2808=ORIENTED_EDGE('',*,*,#2148,.F.);
#2809=ORIENTED_EDGE('',*,*,#2152,.T.);
#2810=ORIENTED_EDGE('',*,*,#2153,.T.);
#2811=ORIENTED_EDGE('',*,*,#2154,.T.);
#2812=ORIENTED_EDGE('',*,*,#2099,.T.);
#2813=ORIENTED_EDGE('',*,*,#2050,.T.);
#2814=ORIENTED_EDGE('',*,*,#2153,.F.);
#2815=ORIENTED_EDGE('',*,*,#2155,.T.);
#2816=ORIENTED_EDGE('',*,*,#2133,.F.);
#2817=ORIENTED_EDGE('',*,*,#2150,.F.);
#2818=ORIENTED_EDGE('',*,*,#2156,.T.);
#2819=ORIENTED_EDGE('',*,*,#2127,.F.);
#2820=ORIENTED_EDGE('',*,*,#2107,.F.);
#2821=ORIENTED_EDGE('',*,*,#2116,.F.);
#2822=ORIENTED_EDGE('',*,*,#2015,.T.);
#2823=ORIENTED_EDGE('',*,*,#2157,.T.);
#2824=ORIENTED_EDGE('',*,*,#2112,.F.);
#2825=ORIENTED_EDGE('',*,*,#2102,.F.);
#2826=ORIENTED_EDGE('',*,*,#2059,.F.);
#2827=ORIENTED_EDGE('',*,*,#2158,.F.);
#2828=ORIENTED_EDGE('',*,*,#2076,.F.);
#2829=ORIENTED_EDGE('',*,*,#2017,.T.);
#2830=ORIENTED_EDGE('',*,*,#2115,.F.);
#2831=ORIENTED_EDGE('',*,*,#2119,.F.);
#2832=ORIENTED_EDGE('',*,*,#2128,.F.);
#2833=ORIENTED_EDGE('',*,*,#2159,.F.);
#2834=ORIENTED_EDGE('',*,*,#2160,.T.);
#2835=ORIENTED_EDGE('',*,*,#2161,.T.);
#2836=ORIENTED_EDGE('',*,*,#1999,.T.);
#2837=ORIENTED_EDGE('',*,*,#2162,.T.);
#2838=ORIENTED_EDGE('',*,*,#2057,.F.);
#2839=ORIENTED_EDGE('',*,*,#2156,.F.);
#2840=ORIENTED_EDGE('',*,*,#2163,.T.);
#2841=ORIENTED_EDGE('',*,*,#2164,.T.);
#2842=ORIENTED_EDGE('',*,*,#2159,.T.);
#2843=ORIENTED_EDGE('',*,*,#2152,.F.);
#2844=ORIENTED_EDGE('',*,*,#2165,.F.);
#2845=ORIENTED_EDGE('',*,*,#2166,.F.);
#2846=ORIENTED_EDGE('',*,*,#2163,.F.);
#2847=ORIENTED_EDGE('',*,*,#2147,.F.);
#2848=ORIENTED_EDGE('',*,*,#2144,.F.);
#2849=ORIENTED_EDGE('',*,*,#2167,.F.);
#2850=ORIENTED_EDGE('',*,*,#2168,.F.);
#2851=ORIENTED_EDGE('',*,*,#2165,.T.);
#2852=ORIENTED_EDGE('',*,*,#2142,.F.);
#2853=ORIENTED_EDGE('',*,*,#2169,.F.);
#2854=ORIENTED_EDGE('',*,*,#2170,.F.);
#2855=ORIENTED_EDGE('',*,*,#2167,.T.);
#2856=ORIENTED_EDGE('',*,*,#2136,.F.);
#2857=ORIENTED_EDGE('',*,*,#2131,.F.);
#2858=ORIENTED_EDGE('',*,*,#2171,.F.);
#2859=ORIENTED_EDGE('',*,*,#2172,.F.);
#2860=ORIENTED_EDGE('',*,*,#2169,.T.);
#2861=ORIENTED_EDGE('',*,*,#2134,.F.);
#2862=ORIENTED_EDGE('',*,*,#2173,.F.);
#2863=ORIENTED_EDGE('',*,*,#2174,.F.);
#2864=ORIENTED_EDGE('',*,*,#2171,.T.);
#2865=ORIENTED_EDGE('',*,*,#2155,.F.);
#2866=ORIENTED_EDGE('',*,*,#2049,.T.);
#2867=ORIENTED_EDGE('',*,*,#2175,.T.);
#2868=ORIENTED_EDGE('',*,*,#2173,.T.);
#2869=ORIENTED_EDGE('',*,*,#1983,.T.);
#2870=ORIENTED_EDGE('',*,*,#2176,.F.);
#2871=ORIENTED_EDGE('',*,*,#2160,.F.);
#2872=ORIENTED_EDGE('',*,*,#2164,.F.);
#2873=ORIENTED_EDGE('',*,*,#2166,.T.);
#2874=ORIENTED_EDGE('',*,*,#2168,.T.);
#2875=ORIENTED_EDGE('',*,*,#2170,.T.);
#2876=ORIENTED_EDGE('',*,*,#2172,.T.);
#2877=ORIENTED_EDGE('',*,*,#2174,.T.);
#2878=ORIENTED_EDGE('',*,*,#2175,.F.);
#2879=ORIENTED_EDGE('',*,*,#2048,.F.);
#2880=ORIENTED_EDGE('',*,*,#2003,.F.);
#2881=ORIENTED_EDGE('',*,*,#1990,.T.);
#2882=ORIENTED_EDGE('',*,*,#1975,.T.);
#2883=ORIENTED_EDGE('',*,*,#2177,.T.);
#2884=ORIENTED_EDGE('',*,*,#2178,.F.);
#2885=ORIENTED_EDGE('',*,*,#2179,.F.);
#2886=ORIENTED_EDGE('',*,*,#2180,.T.);
#2887=ORIENTED_EDGE('',*,*,#2177,.F.);
#2888=ORIENTED_EDGE('',*,*,#2180,.F.);
#2889=ORIENTED_EDGE('',*,*,#2143,.F.);
#2890=ORIENTED_EDGE('',*,*,#2181,.T.);
#2891=ORIENTED_EDGE('',*,*,#2179,.T.);
#2892=ORIENTED_EDGE('',*,*,#2182,.T.);
#2893=ORIENTED_EDGE('',*,*,#2138,.F.);
#2894=ORIENTED_EDGE('',*,*,#2141,.F.);
#2895=ORIENTED_EDGE('',*,*,#2078,.F.);
#2896=ORIENTED_EDGE('',*,*,#2093,.T.);
#2897=ORIENTED_EDGE('',*,*,#2183,.T.);
#2898=ORIENTED_EDGE('',*,*,#2052,.T.);
#2899=ORIENTED_EDGE('',*,*,#2079,.F.);
#2900=ORIENTED_EDGE('',*,*,#2051,.T.);
#2901=ORIENTED_EDGE('',*,*,#2098,.F.);
#2902=ORIENTED_EDGE('',*,*,#2088,.F.);
#2903=ORIENTED_EDGE('',*,*,#2184,.T.);
#2904=ORIENTED_EDGE('',*,*,#2080,.F.);
#2905=ORIENTED_EDGE('',*,*,#2085,.F.);
#2906=ORIENTED_EDGE('',*,*,#2184,.F.);
#2907=ORIENTED_EDGE('',*,*,#2185,.T.);
#2908=ORIENTED_EDGE('',*,*,#2061,.F.);
#2909=ORIENTED_EDGE('',*,*,#2073,.T.);
#2910=ORIENTED_EDGE('',*,*,#2068,.F.);
#2911=ORIENTED_EDGE('',*,*,#2071,.F.);
#2912=ORIENTED_EDGE('',*,*,#2158,.T.);
#2913=ORIENTED_EDGE('',*,*,#2072,.F.);
#2914=ORIENTED_EDGE('',*,*,#2045,.F.);
#2915=ORIENTED_EDGE('',*,*,#2186,.T.);
#2916=ORIENTED_EDGE('',*,*,#2187,.T.);
#2917=ORIENTED_EDGE('',*,*,#2186,.F.);
#2918=ORIENTED_EDGE('',*,*,#2031,.F.);
#2919=ORIENTED_EDGE('',*,*,#2043,.F.);
#2920=ORIENTED_EDGE('',*,*,#2188,.T.);
#2921=ORIENTED_EDGE('',*,*,#2012,.T.);
#2922=ORIENTED_EDGE('',*,*,#2023,.F.);
#2923=ORIENTED_EDGE('',*,*,#2027,.F.);
#2924=ORIENTED_EDGE('',*,*,#2074,.F.);
#2925=ORIENTED_EDGE('',*,*,#2189,.T.);
#2926=ORIENTED_EDGE('',*,*,#2020,.T.);
#2927=ORIENTED_EDGE('',*,*,#2189,.F.);
#2928=ORIENTED_EDGE('',*,*,#2185,.F.);
#2929=ORIENTED_EDGE('',*,*,#2190,.T.);
#2930=ORIENTED_EDGE('',*,*,#2191,.T.);
#2931=ORIENTED_EDGE('',*,*,#2190,.F.);
#2932=ORIENTED_EDGE('',*,*,#2122,.F.);
#2933=ORIENTED_EDGE('',*,*,#2192,.T.);
#2934=ORIENTED_EDGE('',*,*,#2021,.T.);
#2935=ORIENTED_EDGE('',*,*,#2192,.F.);
#2936=ORIENTED_EDGE('',*,*,#2113,.F.);
#2937=ORIENTED_EDGE('',*,*,#2157,.F.);
#2938=ORIENTED_EDGE('',*,*,#2193,.T.);
#2939=ORIENTED_EDGE('',*,*,#2123,.F.);
#2940=ORIENTED_EDGE('',*,*,#2120,.F.);
#2941=ORIENTED_EDGE('',*,*,#2194,.F.);
#2942=ORIENTED_EDGE('',*,*,#2195,.T.);
#2943=ORIENTED_EDGE('',*,*,#2195,.F.);
#2944=ORIENTED_EDGE('',*,*,#2002,.F.);
#2945=ORIENTED_EDGE('',*,*,#2196,.T.);
#2946=ORIENTED_EDGE('',*,*,#2194,.T.);
#2947=ORIENTED_EDGE('',*,*,#2196,.F.);
#2948=ORIENTED_EDGE('',*,*,#2197,.F.);
#2949=ORIENTED_EDGE('',*,*,#2198,.T.);
#2950=ORIENTED_EDGE('',*,*,#2198,.F.);
#2951=ORIENTED_EDGE('',*,*,#2001,.F.);
#2952=ORIENTED_EDGE('',*,*,#2199,.T.);
#2953=ORIENTED_EDGE('',*,*,#2197,.T.);
#2954=ORIENTED_EDGE('',*,*,#2199,.F.);
#2955=ORIENTED_EDGE('',*,*,#1982,.T.);
#2956=ORIENTED_EDGE('',*,*,#2000,.F.);
#2957=ORIENTED_EDGE('',*,*,#2161,.F.);
#2958=ORIENTED_EDGE('',*,*,#2176,.T.);
#2959=ORIENTED_EDGE('',*,*,#2034,.F.);
#2960=ORIENTED_EDGE('',*,*,#2200,.F.);
#2961=ORIENTED_EDGE('',*,*,#2054,.F.);
#2962=ORIENTED_EDGE('',*,*,#2162,.F.);
#2963=ORIENTED_EDGE('',*,*,#1998,.T.);
#2964=ORIENTED_EDGE('',*,*,#2047,.F.);
#2965=ORIENTED_EDGE('',*,*,#2037,.F.);
#2966=ORIENTED_EDGE('',*,*,#2009,.F.);
#2967=ORIENTED_EDGE('',*,*,#2055,.F.);
#2968=ORIENTED_EDGE('',*,*,#2200,.T.);
#2969=ORIENTED_EDGE('',*,*,#1971,.T.);
#2970=ORIENTED_EDGE('',*,*,#2013,.T.);
#2971=ORIENTED_EDGE('',*,*,#2188,.F.);
#2972=ORIENTED_EDGE('',*,*,#2042,.F.);
#2973=ORIENTED_EDGE('',*,*,#2053,.F.);
#2974=ORIENTED_EDGE('',*,*,#2183,.F.);
#2975=ORIENTED_EDGE('',*,*,#2092,.F.);
#2976=ORIENTED_EDGE('',*,*,#2201,.F.);
#2977=ORIENTED_EDGE('',*,*,#2187,.F.);
#2978=ORIENTED_EDGE('',*,*,#2191,.F.);
#2979=ORIENTED_EDGE('',*,*,#1972,.T.);
#2980=ORIENTED_EDGE('',*,*,#2201,.T.);
#2981=ORIENTED_EDGE('',*,*,#2096,.F.);
#2982=ORIENTED_EDGE('',*,*,#2100,.F.);
#2983=ORIENTED_EDGE('',*,*,#2154,.F.);
#2984=ORIENTED_EDGE('',*,*,#2135,.F.);
#2985=ORIENTED_EDGE('',*,*,#2129,.F.);
#2986=ORIENTED_EDGE('',*,*,#2139,.F.);
#2987=ORIENTED_EDGE('',*,*,#2182,.F.);
#2988=ORIENTED_EDGE('',*,*,#2178,.T.);
#2989=ORIENTED_EDGE('',*,*,#2181,.F.);
#2990=ORIENTED_EDGE('',*,*,#2146,.F.);
#2991=ORIENTED_EDGE('',*,*,#2149,.F.);
#2992=ORIENTED_EDGE('',*,*,#2151,.F.);
#2993=ORIENTED_EDGE('',*,*,#2126,.F.);
#2994=ORIENTED_EDGE('',*,*,#2124,.F.);
#2995=ORIENTED_EDGE('',*,*,#2193,.F.);
#2996=ORIENTED_EDGE('',*,*,#2014,.T.);
#2997=ORIENTED_EDGE('',*,*,#1969,.T.);
#2998=ORIENTED_EDGE('',*,*,#1966,.T.);
#2999=ORIENTED_EDGE('',*,*,#1984,.T.);
#3000=ORIENTED_EDGE('',*,*,#1977,.T.);
#3001=ORIENTED_EDGE('',*,*,#1989,.T.);
#3002=ORIENTED_EDGE('',*,*,#1986,.T.);
#3653=PLANE('',#4113);
#3654=PLANE('',#4114);
#3655=PLANE('',#4115);
#3656=PLANE('',#4116);
#3657=PLANE('',#4117);
#3658=PLANE('',#4118);
#3659=PLANE('',#4119);
#3660=PLANE('',#4120);
#3661=PLANE('',#4121);
#3662=PLANE('',#4124);
#3663=PLANE('',#4125);
#3664=PLANE('',#4128);
#3665=PLANE('',#4154);
#3666=PLANE('',#4157);
#3667=PLANE('',#4175);
#3668=PLANE('',#4189);
#3669=PLANE('',#4190);
#3670=PLANE('',#4205);
#3671=PLANE('',#4206);
#3672=PLANE('',#4239);
#3673=PLANE('',#4242);
#3674=PLANE('',#4249);
#3675=PLANE('',#4252);
#3676=PLANE('',#4257);
#3677=PLANE('',#4261);
#3678=PLANE('',#4272);
#3679=PLANE('',#4279);
#3680=PLANE('',#4280);
#3681=PLANE('',#4282);
#3682=PLANE('',#4283);
#3767=ADVANCED_FACE('',(#526),#3653,.F.);
#3768=ADVANCED_FACE('',(#527),#3654,.F.);
#3769=ADVANCED_FACE('',(#528),#3655,.F.);
#3770=ADVANCED_FACE('',(#529),#3656,.F.);
#3771=ADVANCED_FACE('',(#530),#3657,.F.);
#3772=ADVANCED_FACE('',(#531),#3658,.F.);
#3773=ADVANCED_FACE('',(#532),#3659,.F.);
#3774=ADVANCED_FACE('',(#533),#3660,.F.);
#3775=ADVANCED_FACE('',(#534,#337,#338),#3661,.T.);
#3776=ADVANCED_FACE('',(#535),#3662,.T.);
#3777=ADVANCED_FACE('',(#536),#3663,.T.);
#3778=ADVANCED_FACE('',(#537,#339,#340),#3664,.T.);
#3779=ADVANCED_FACE('',(#538),#300,.F.);
#3780=ADVANCED_FACE('',(#539),#193,.T.);
#3781=ADVANCED_FACE('',(#540),#301,.F.);
#3782=ADVANCED_FACE('',(#541),#302,.F.);
#3783=ADVANCED_FACE('',(#542),#194,.T.);
#3784=ADVANCED_FACE('',(#543),#104,.T.);
#3785=ADVANCED_FACE('',(#544),#195,.T.);
#3786=ADVANCED_FACE('',(#545),#105,.F.);
#3787=ADVANCED_FACE('',(#546,#341),#3665,.T.);
#3788=ADVANCED_FACE('',(#547),#106,.F.);
#3789=ADVANCED_FACE('',(#548),#3666,.T.);
#3790=ADVANCED_FACE('',(#549),#196,.T.);
#3791=ADVANCED_FACE('',(#550),#107,.T.);
#3792=ADVANCED_FACE('',(#551),#303,.F.);
#3793=ADVANCED_FACE('',(#552),#197,.T.);
#3794=ADVANCED_FACE('',(#553),#304,.F.);
#3795=ADVANCED_FACE('',(#554),#305,.F.);
#3796=ADVANCED_FACE('',(#555),#198,.T.);
#3797=ADVANCED_FACE('',(#556,#342),#3667,.T.);
#3798=ADVANCED_FACE('',(#557),#108,.F.);
#3799=ADVANCED_FACE('',(#558),#109,.T.);
#3800=ADVANCED_FACE('',(#559),#306,.F.);
#3801=ADVANCED_FACE('',(#560),#307,.F.);
#3802=ADVANCED_FACE('',(#561),#199,.T.);
#3803=ADVANCED_FACE('',(#562),#308,.F.);
#3804=ADVANCED_FACE('',(#563),#110,.T.);
#3805=ADVANCED_FACE('',(#564),#3668,.T.);
#3806=ADVANCED_FACE('',(#565),#3669,.T.);
#3807=ADVANCED_FACE('',(#566),#309,.F.);
#3808=ADVANCED_FACE('',(#567),#200,.T.);
#3809=ADVANCED_FACE('',(#568),#310,.F.);
#3810=ADVANCED_FACE('',(#569),#311,.F.);
#3811=ADVANCED_FACE('',(#570),#312,.F.);
#3812=ADVANCED_FACE('',(#571),#111,.F.);
#3813=ADVANCED_FACE('',(#572),#112,.F.);
#3814=ADVANCED_FACE('',(#573),#3670,.T.);
#3815=ADVANCED_FACE('',(#574,#343),#3671,.T.);
#3816=ADVANCED_FACE('',(#575),#313,.F.);
#3817=ADVANCED_FACE('',(#576),#113,.T.);
#3818=ADVANCED_FACE('',(#577),#201,.T.);
#3819=ADVANCED_FACE('',(#578),#114,.T.);
#3820=ADVANCED_FACE('',(#579),#314,.F.);
#3821=ADVANCED_FACE('',(#580),#315,.F.);
#3822=ADVANCED_FACE('',(#581),#316,.F.);
#3823=ADVANCED_FACE('',(#582),#202,.T.);
#3824=ADVANCED_FACE('',(#583),#115,.T.);
#3825=ADVANCED_FACE('',(#584),#116,.T.);
#3826=ADVANCED_FACE('',(#585),#102,.T.);
#3827=ADVANCED_FACE('',(#586),#103,.T.);
#3828=ADVANCED_FACE('',(#587),#117,.T.);
#3829=ADVANCED_FACE('',(#588),#3672,.F.);
#3830=ADVANCED_FACE('',(#589),#118,.T.);
#3831=ADVANCED_FACE('',(#590),#3673,.F.);
#3832=ADVANCED_FACE('',(#591),#119,.F.);
#3833=ADVANCED_FACE('',(#592),#120,.T.);
#3834=ADVANCED_FACE('',(#593),#121,.F.);
#3835=ADVANCED_FACE('',(#594),#3674,.F.);
#3836=ADVANCED_FACE('',(#595),#122,.T.);
#3837=ADVANCED_FACE('',(#596,#344),#3675,.T.);
#3838=ADVANCED_FACE('',(#597),#123,.F.);
#3839=ADVANCED_FACE('',(#598),#3676,.T.);
#3840=ADVANCED_FACE('',(#599),#124,.F.);
#3841=ADVANCED_FACE('',(#600),#125,.F.);
#3842=ADVANCED_FACE('',(#601,#345),#3677,.T.);
#3843=ADVANCED_FACE('',(#602),#126,.F.);
#3844=ADVANCED_FACE('',(#603),#127,.F.);
#3845=ADVANCED_FACE('',(#604),#128,.T.);
#3846=ADVANCED_FACE('',(#605),#129,.F.);
#3847=ADVANCED_FACE('',(#606),#130,.F.);
#3848=ADVANCED_FACE('',(#607),#131,.F.);
#3849=ADVANCED_FACE('',(#608),#3678,.T.);
#3850=ADVANCED_FACE('',(#609),#99,.F.);
#3851=ADVANCED_FACE('',(#610),#132,.F.);
#3852=ADVANCED_FACE('',(#611),#100,.F.);
#3853=ADVANCED_FACE('',(#612),#133,.F.);
#3854=ADVANCED_FACE('',(#613),#3679,.T.);
#3855=ADVANCED_FACE('',(#614),#3680,.T.);
#3856=ADVANCED_FACE('',(#615),#134,.T.);
#3857=ADVANCED_FACE('',(#616,#346,#347),#3681,.T.);
#3858=ADVANCED_FACE('',(#617),#3682,.T.);
#4002=CLOSED_SHELL('',(#3767,#3768,#3769,#3770,#3771,#3772,#3773,#3774,
#3775,#3776,#3777,#3778,#3779,#3780,#3781,#3782,#3783,#3784,#3785,#3786,
#3787,#3788,#3789,#3790,#3791,#3792,#3793,#3794,#3795,#3796,#3797,#3798,
#3799,#3800,#3801,#3802,#3803,#3804,#3805,#3806,#3807,#3808,#3809,#3810,
#3811,#3812,#3813,#3814,#3815,#3816,#3817,#3818,#3819,#3820,#3821,#3822,
#3823,#3824,#3825,#3826,#3827,#3828,#3829,#3830,#3831,#3832,#3833,#3834,
#3835,#3836,#3837,#3838,#3839,#3840,#3841,#3842,#3843,#3844,#3845,#3846,
#3847,#3848,#3849,#3850,#3851,#3852,#3853,#3854,#3855,#3856,#3857,#3858));
#4112=AXIS2_PLACEMENT_3D('',#5607,#4515,#4516);
#4113=AXIS2_PLACEMENT_3D('',#5608,#4517,#4518);
#4114=AXIS2_PLACEMENT_3D('',#5617,#4523,#4524);
#4115=AXIS2_PLACEMENT_3D('',#5623,#4528,#4529);
#4116=AXIS2_PLACEMENT_3D('',#5632,#4534,#4535);
#4117=AXIS2_PLACEMENT_3D('',#5641,#4540,#4541);
#4118=AXIS2_PLACEMENT_3D('',#5652,#4548,#4549);
#4119=AXIS2_PLACEMENT_3D('',#5658,#4553,#4554);
#4120=AXIS2_PLACEMENT_3D('',#5669,#4561,#4562);
#4121=AXIS2_PLACEMENT_3D('',#5672,#4565,#4566);
#4122=AXIS2_PLACEMENT_3D('',#5683,#4572,#4573);
#4123=AXIS2_PLACEMENT_3D('',#5685,#4574,#4575);
#4124=AXIS2_PLACEMENT_3D('',#5686,#4576,#4577);
#4125=AXIS2_PLACEMENT_3D('',#5690,#4580,#4581);
#4126=AXIS2_PLACEMENT_3D('',#5696,#4584,#4585);
#4127=AXIS2_PLACEMENT_3D('',#5704,#4589,#4590);
#4128=AXIS2_PLACEMENT_3D('',#5708,#4593,#4594);
#4129=AXIS2_PLACEMENT_3D('',#5712,#4596,#4597);
#4130=AXIS2_PLACEMENT_3D('',#5714,#4598,#4599);
#4131=AXIS2_PLACEMENT_3D('',#5718,#4601,#4602);
#4132=AXIS2_PLACEMENT_3D('',#5719,#4603,#4604);
#4133=AXIS2_PLACEMENT_3D('',#5721,#4605,#4606);
#4134=AXIS2_PLACEMENT_3D('',#5723,#4607,#4608);
#4135=AXIS2_PLACEMENT_3D('',#5746,#4609,#4610);
#4136=AXIS2_PLACEMENT_3D('',#5752,#4611,#4612);
#4137=AXIS2_PLACEMENT_3D('',#5757,#4613,#4614);
#4138=AXIS2_PLACEMENT_3D('',#5760,#4615,#4616);
#4139=AXIS2_PLACEMENT_3D('',#5761,#4617,#4618);
#4140=AXIS2_PLACEMENT_3D('',#5762,#4619,#4620);
#4141=AXIS2_PLACEMENT_3D('',#5789,#4621,#4622);
#4142=AXIS2_PLACEMENT_3D('',#5830,#4623,#4624);
#4143=AXIS2_PLACEMENT_3D('',#5831,#4625,#4626);
#4144=AXIS2_PLACEMENT_3D('',#5832,#4627,#4628);
#4145=AXIS2_PLACEMENT_3D('',#5850,#4629,#4630);
#4146=AXIS2_PLACEMENT_3D('',#5851,#4631,#4632);
#4147=AXIS2_PLACEMENT_3D('',#5852,#4633,#4634);
#4148=AXIS2_PLACEMENT_3D('',#5853,#4635,#4636);
#4149=AXIS2_PLACEMENT_3D('',#5855,#4637,#4638);
#4150=AXIS2_PLACEMENT_3D('',#5857,#4640,#4641);
#4151=AXIS2_PLACEMENT_3D('',#5858,#4642,#4643);
#4152=AXIS2_PLACEMENT_3D('',#5859,#4644,#4645);
#4153=AXIS2_PLACEMENT_3D('',#5863,#4647,#4648);
#4154=AXIS2_PLACEMENT_3D('',#5865,#4650,#4651);
#4155=AXIS2_PLACEMENT_3D('',#5868,#4653,#4654);
#4156=AXIS2_PLACEMENT_3D('',#5869,#4655,#4656);
#4157=AXIS2_PLACEMENT_3D('',#5871,#4658,#4659);
#4158=AXIS2_PLACEMENT_3D('',#5884,#4667,#4668);
#4159=AXIS2_PLACEMENT_3D('',#5901,#4669,#4670);
#4160=AXIS2_PLACEMENT_3D('',#5903,#4671,#4672);
#4161=AXIS2_PLACEMENT_3D('',#5904,#4673,#4674);
#4162=AXIS2_PLACEMENT_3D('',#5905,#4675,#4676);
#4163=AXIS2_PLACEMENT_3D('',#5907,#4677,#4678);
#4164=AXIS2_PLACEMENT_3D('',#5931,#4680,#4681);
#4165=AXIS2_PLACEMENT_3D('',#5937,#4682,#4683);
#4166=AXIS2_PLACEMENT_3D('',#5942,#4684,#4685);
#4167=AXIS2_PLACEMENT_3D('',#5945,#4686,#4687);
#4168=AXIS2_PLACEMENT_3D('',#5946,#4688,#4689);
#4169=AXIS2_PLACEMENT_3D('',#5947,#4690,#4691);
#4170=AXIS2_PLACEMENT_3D('',#5970,#4692,#4693);
#4171=AXIS2_PLACEMENT_3D('',#6010,#4694,#4695);
#4172=AXIS2_PLACEMENT_3D('',#6011,#4696,#4697);
#4173=AXIS2_PLACEMENT_3D('',#6012,#4698,#4699);
#4174=AXIS2_PLACEMENT_3D('',#6013,#4700,#4701);
#4175=AXIS2_PLACEMENT_3D('',#6014,#4702,#4703);
#4176=AXIS2_PLACEMENT_3D('',#6017,#4705,#4706);
#4177=AXIS2_PLACEMENT_3D('',#6018,#4707,#4708);
#4178=AXIS2_PLACEMENT_3D('',#6021,#4711,#4712);
#4179=AXIS2_PLACEMENT_3D('',#6054,#4713,#4714);
#4180=AXIS2_PLACEMENT_3D('',#6055,#4715,#4716);
#4181=AXIS2_PLACEMENT_3D('',#6056,#4717,#4718);
#4182=AXIS2_PLACEMENT_3D('',#6083,#4719,#4720);
#4183=AXIS2_PLACEMENT_3D('',#6088,#4721,#4722);
#4184=AXIS2_PLACEMENT_3D('',#6091,#4723,#4724);
#4185=AXIS2_PLACEMENT_3D('',#6092,#4725,#4726);
#4186=AXIS2_PLACEMENT_3D('',#6093,#4727,#4728);
#4187=AXIS2_PLACEMENT_3D('',#6150,#4729,#4730);
#4188=AXIS2_PLACEMENT_3D('',#6154,#4732,#4733);
#4189=AXIS2_PLACEMENT_3D('',#6156,#4735,#4736);
#4190=AXIS2_PLACEMENT_3D('',#6167,#4739,#4740);
#4191=AXIS2_PLACEMENT_3D('',#6199,#4741,#4742);
#4192=AXIS2_PLACEMENT_3D('',#6201,#4743,#4744);
#4193=AXIS2_PLACEMENT_3D('',#6202,#4745,#4746);
#4194=AXIS2_PLACEMENT_3D('',#6203,#4747,#4748);
#4195=AXIS2_PLACEMENT_3D('',#6206,#4749,#4750);
#4196=AXIS2_PLACEMENT_3D('',#6208,#4751,#4752);
#4197=AXIS2_PLACEMENT_3D('',#6210,#4753,#4754);
#4198=AXIS2_PLACEMENT_3D('',#6211,#4755,#4756);
#4199=AXIS2_PLACEMENT_3D('',#6238,#4757,#4758);
#4200=AXIS2_PLACEMENT_3D('',#6279,#4759,#4760);
#4201=AXIS2_PLACEMENT_3D('',#6280,#4761,#4762);
#4202=AXIS2_PLACEMENT_3D('',#6338,#4763,#4764);
#4203=AXIS2_PLACEMENT_3D('',#6341,#4767,#4768);
#4204=AXIS2_PLACEMENT_3D('',#6344,#4770,#4771);
#4205=AXIS2_PLACEMENT_3D('',#6346,#4773,#4774);
#4206=AXIS2_PLACEMENT_3D('',#6355,#4776,#4777);
#4207=AXIS2_PLACEMENT_3D('',#6357,#4778,#4779);
#4208=AXIS2_PLACEMENT_3D('',#6391,#4780,#4781);
#4209=AXIS2_PLACEMENT_3D('',#6392,#4782,#4783);
#4210=AXIS2_PLACEMENT_3D('',#6393,#4784,#4785);
#4211=AXIS2_PLACEMENT_3D('',#6397,#4787,#4788);
#4212=AXIS2_PLACEMENT_3D('',#6399,#4790,#4791);
#4213=AXIS2_PLACEMENT_3D('',#6402,#4792,#4793);
#4214=AXIS2_PLACEMENT_3D('',#6404,#4794,#4795);
#4215=AXIS2_PLACEMENT_3D('',#6406,#4796,#4797);
#4216=AXIS2_PLACEMENT_3D('',#6419,#4798,#4799);
#4217=AXIS2_PLACEMENT_3D('',#6422,#4800,#4801);
#4218=AXIS2_PLACEMENT_3D('',#6446,#4804,#4805);
#4219=AXIS2_PLACEMENT_3D('',#6448,#4806,#4807);
#4220=AXIS2_PLACEMENT_3D('',#6450,#4808,#4809);
#4221=AXIS2_PLACEMENT_3D('',#6510,#4810,#4811);
#4222=AXIS2_PLACEMENT_3D('',#6511,#4812,#4813);
#4223=AXIS2_PLACEMENT_3D('',#6512,#4814,#4815);
#4224=AXIS2_PLACEMENT_3D('',#6534,#4816,#4817);
#4225=AXIS2_PLACEMENT_3D('',#6536,#4818,#4819);
#4226=AXIS2_PLACEMENT_3D('',#6600,#4820,#4821);
#4227=AXIS2_PLACEMENT_3D('',#6602,#4822,#4823);
#4228=AXIS2_PLACEMENT_3D('',#6604,#4824,#4825);
#4229=AXIS2_PLACEMENT_3D('',#6605,#4826,#4827);
#4230=AXIS2_PLACEMENT_3D('',#6606,#4828,#4829);
#4231=AXIS2_PLACEMENT_3D('',#6608,#4830,#4831);
#4232=AXIS2_PLACEMENT_3D('',#6611,#4834,#4835);
#4233=AXIS2_PLACEMENT_3D('',#6612,#4836,#4837);
#4234=AXIS2_PLACEMENT_3D('',#6614,#4839,#4840);
#4235=AXIS2_PLACEMENT_3D('',#6615,#4841,#4842);
#4236=AXIS2_PLACEMENT_3D('',#6616,#4843,#4844);
#4237=AXIS2_PLACEMENT_3D('',#6617,#4845,#4846);
#4238=AXIS2_PLACEMENT_3D('',#6618,#4847,#4848);
#4239=AXIS2_PLACEMENT_3D('',#6620,#4850,#4851);
#4240=AXIS2_PLACEMENT_3D('',#6628,#4857,#4858);
#4241=AXIS2_PLACEMENT_3D('',#6631,#4860,#4861);
#4242=AXIS2_PLACEMENT_3D('',#6632,#4862,#4863);
#4243=AXIS2_PLACEMENT_3D('',#6636,#4866,#4867);
#4244=AXIS2_PLACEMENT_3D('',#6639,#4869,#4870);
#4245=AXIS2_PLACEMENT_3D('',#6640,#4871,#4872);
#4246=AXIS2_PLACEMENT_3D('',#6643,#4874,#4875);
#4247=AXIS2_PLACEMENT_3D('',#6644,#4876,#4877);
#4248=AXIS2_PLACEMENT_3D('',#6647,#4879,#4880);
#4249=AXIS2_PLACEMENT_3D('',#6648,#4881,#4882);
#4250=AXIS2_PLACEMENT_3D('',#6652,#4885,#4886);
#4251=AXIS2_PLACEMENT_3D('',#6653,#4887,#4888);
#4252=AXIS2_PLACEMENT_3D('',#6654,#4889,#4890);
#4253=AXIS2_PLACEMENT_3D('',#6657,#4892,#4893);
#4254=AXIS2_PLACEMENT_3D('',#6658,#4894,#4895);
#4255=AXIS2_PLACEMENT_3D('',#6661,#4896,#4897);
#4256=AXIS2_PLACEMENT_3D('',#6662,#4898,#4899);
#4257=AXIS2_PLACEMENT_3D('',#6664,#4901,#4902);
#4258=AXIS2_PLACEMENT_3D('',#6667,#4905,#4906);
#4259=AXIS2_PLACEMENT_3D('',#6668,#4907,#4908);
#4260=AXIS2_PLACEMENT_3D('',#6669,#4909,#4910);
#4261=AXIS2_PLACEMENT_3D('',#6671,#4912,#4913);
#4262=AXIS2_PLACEMENT_3D('',#6673,#4914,#4915);
#4263=AXIS2_PLACEMENT_3D('',#6674,#4916,#4917);
#4264=AXIS2_PLACEMENT_3D('',#6675,#4918,#4919);
#4265=AXIS2_PLACEMENT_3D('',#6678,#4921,#4922);
#4266=AXIS2_PLACEMENT_3D('',#6679,#4923,#4924);
#4267=AXIS2_PLACEMENT_3D('',#6680,#4925,#4926);
#4268=AXIS2_PLACEMENT_3D('',#6681,#4927,#4928);
#4269=AXIS2_PLACEMENT_3D('',#6683,#4930,#4931);
#4270=AXIS2_PLACEMENT_3D('',#6686,#4933,#4934);
#4271=AXIS2_PLACEMENT_3D('',#6687,#4935,#4936);
#4272=AXIS2_PLACEMENT_3D('',#6689,#4938,#4939);
#4273=AXIS2_PLACEMENT_3D('',#6691,#4941,#4942);
#4274=AXIS2_PLACEMENT_3D('',#6693,#4943,#4944);
#4275=AXIS2_PLACEMENT_3D('',#6696,#4946,#4947);
#4276=AXIS2_PLACEMENT_3D('',#6698,#4949,#4950);
#4277=AXIS2_PLACEMENT_3D('',#6700,#4951,#4952);
#4278=AXIS2_PLACEMENT_3D('',#6703,#4954,#4955);
#4279=AXIS2_PLACEMENT_3D('',#6705,#4957,#4958);
#4280=AXIS2_PLACEMENT_3D('',#6706,#4959,#4960);
#4281=AXIS2_PLACEMENT_3D('',#6708,#4962,#4963);
#4282=AXIS2_PLACEMENT_3D('',#6709,#4964,#4965);
#4283=AXIS2_PLACEMENT_3D('',#6711,#4967,#4968);
#4515=DIRECTION('axis',(0.,0.,1.));
#4516=DIRECTION('refdir',(1.,0.,0.));
#4517=DIRECTION('center_axis',(-0.00925888381263175,0.,0.999957135616594));
#4518=DIRECTION('ref_axis',(0.,1.,0.));
#4519=DIRECTION('',(0.,-1.,0.));
#4520=DIRECTION('',(-0.999957135616594,0.,-0.00925888381263175));
#4521=DIRECTION('',(0.,1.,0.));
#4522=DIRECTION('',(-0.999957135616594,0.,-0.00925888381263175));
#4523=DIRECTION('center_axis',(0.,-1.,0.));
#4524=DIRECTION('ref_axis',(-0.00925888381263175,0.,0.999957135616594));
#4525=DIRECTION('',(0.,0.,-1.));
#4526=DIRECTION('',(-0.00925888381263175,0.,0.999957135616594));
#4527=DIRECTION('',(1.,0.,0.));
#4528=DIRECTION('center_axis',(0.,1.,0.));
#4529=DIRECTION('ref_axis',(0.00925888381263175,0.,-0.999957135616594));
#4530=DIRECTION('',(-1.,0.,0.));
#4531=DIRECTION('',(0.00925888381263175,0.,-0.999957135616594));
#4532=DIRECTION('',(-0.999957135616594,0.,-0.00925888381263175));
#4533=DIRECTION('',(0.,0.,1.));
#4534=DIRECTION('center_axis',(-0.00925888381263175,0.,0.999957135616594));
#4535=DIRECTION('ref_axis',(0.,1.,0.));
#4536=DIRECTION('',(0.,-1.,0.));
#4537=DIRECTION('',(-0.999957135616594,0.,-0.00925888381263175));
#4538=DIRECTION('',(0.,1.,0.));
#4539=DIRECTION('',(-0.999957135616594,0.,-0.00925888381263175));
#4540=DIRECTION('center_axis',(0.,-1.,0.));
#4541=DIRECTION('ref_axis',(-0.00925888381263175,0.,0.999957135616594));
#4542=DIRECTION('',(0.,0.,-1.));
#4543=DIRECTION('',(-0.999957135616594,0.,-0.00925888381263175));
#4544=DIRECTION('',(0.,0.,1.));
#4545=DIRECTION('',(-1.,0.,0.));
#4546=DIRECTION('',(0.,0.,-1.));
#4547=DIRECTION('',(-0.00925888381263175,0.,0.999957135616594));
#4548=DIRECTION('center_axis',(-0.00925888381263175,0.,0.999957135616594));
#4549=DIRECTION('ref_axis',(0.,1.,0.));
#4550=DIRECTION('',(0.,-1.,0.));
#4551=DIRECTION('',(0.,1.,0.));
#4552=DIRECTION('',(-0.999957135616594,0.,-0.00925888381263175));
#4553=DIRECTION('center_axis',(0.,1.,0.));
#4554=DIRECTION('ref_axis',(0.00925888381263175,0.,-0.999957135616594));
#4555=DIRECTION('',(0.,0.,1.));
#4556=DIRECTION('',(0.00925888381263175,0.,-0.999957135616594));
#4557=DIRECTION('',(0.,0.,1.));
#4558=DIRECTION('',(1.,0.,0.));
#4559=DIRECTION('',(0.,0.,-1.));
#4560=DIRECTION('',(-0.999957135616594,0.,-0.00925888381263175));
#4561=DIRECTION('center_axis',(-0.00925888381263175,0.,0.999957135616594));
#4562=DIRECTION('ref_axis',(0.,1.,0.));
#4563=DIRECTION('',(0.,-1.,0.));
#4564=DIRECTION('',(0.,1.,0.));
#4565=DIRECTION('center_axis',(1.,0.,0.));
#4566=DIRECTION('ref_axis',(0.,0.,-1.));
#4567=DIRECTION('',(0.,1.,0.));
#4568=DIRECTION('',(0.,0.,-1.));
#4569=DIRECTION('',(0.,1.,0.));
#4570=DIRECTION('',(0.,0.,1.));
#4571=DIRECTION('',(0.,1.,0.));
#4572=DIRECTION('center_axis',(-1.,0.,0.));
#4573=DIRECTION('ref_axis',(0.,1.,0.));
#4574=DIRECTION('center_axis',(-1.,0.,0.));
#4575=DIRECTION('ref_axis',(0.,1.,0.));
#4576=DIRECTION('center_axis',(0.,0.,1.));
#4577=DIRECTION('ref_axis',(1.,0.,0.));
#4578=DIRECTION('',(0.,1.,0.));
#4579=DIRECTION('',(1.,0.,0.));
#4580=DIRECTION('center_axis',(-1.,0.,0.));
#4581=DIRECTION('ref_axis',(0.,0.,1.));
#4582=DIRECTION('',(0.,1.,0.));
#4583=DIRECTION('',(0.,0.,-1.));
#4584=DIRECTION('center_axis',(-1.,0.,0.));
#4585=DIRECTION('ref_axis',(0.,1.,0.));
#4586=DIRECTION('',(0.,0.,-1.));
#4587=DIRECTION('',(0.,1.,0.));
#4588=DIRECTION('',(0.,0.,1.));
#4589=DIRECTION('center_axis',(-1.,0.,0.));
#4590=DIRECTION('ref_axis',(0.,-1.,0.));
#4591=DIRECTION('',(0.,0.,1.));
#4592=DIRECTION('',(0.,1.,0.));
#4593=DIRECTION('center_axis',(0.,0.,-1.));
#4594=DIRECTION('ref_axis',(-1.,0.,0.));
#4595=DIRECTION('',(0.,1.,0.));
#4596=DIRECTION('center_axis',(0.,0.,1.));
#4597=DIRECTION('ref_axis',(-1.,0.,0.));
#4598=DIRECTION('center_axis',(0.,0.,-1.));
#4599=DIRECTION('ref_axis',(0.67202150503225,0.740531631177352,0.));
#4600=DIRECTION('',(1.,0.,0.));
#4601=DIRECTION('center_axis',(0.,0.,-1.));
#4602=DIRECTION('ref_axis',(-0.67202150503225,0.740531631177352,0.));
#4603=DIRECTION('center_axis',(0.,0.,1.));
#4604=DIRECTION('ref_axis',(-1.,0.,0.));
#4605=DIRECTION('center_axis',(0.,0.,-1.));
#4606=DIRECTION('ref_axis',(1.,0.,0.));
#4607=DIRECTION('center_axis',(0.,0.,-1.));
#4608=DIRECTION('ref_axis',(1.,0.,0.));
#4609=DIRECTION('center_axis',(-0.120000000000002,-0.992773891679268,-5.92281122919324E-15));
#4610=DIRECTION('ref_axis',(-3.70074341541719E-16,-5.9211894646675E-15,
1.));
#4611=DIRECTION('center_axis',(6.53807313370374E-14,0.866025403784389,-0.500000000000086));
#4612=DIRECTION('ref_axis',(-1.,7.54951656745106E-14,0.));
#4613=DIRECTION('center_axis',(0.,0.,1.));
#4614=DIRECTION('ref_axis',(1.,0.,0.));
#4615=DIRECTION('center_axis',(-0.119999999999998,0.992773891679269,0.));
#4616=DIRECTION('ref_axis',(0.,0.,1.));
#4617=DIRECTION('center_axis',(0.,0.,1.));
#4618=DIRECTION('ref_axis',(-1.58603289232165E-16,1.,0.));
#4619=DIRECTION('center_axis',(0.,0.,-1.));
#4620=DIRECTION('ref_axis',(-1.58603289232165E-16,1.,0.));
#4621=DIRECTION('center_axis',(-0.0963241948601912,0.990678201521095,-0.0963241948601896));
#4622=DIRECTION('ref_axis',(0.,0.0967741935483864,0.995306362615581));
#4623=DIRECTION('center_axis',(-0.447213595499958,0.,0.894427190999916));
#4624=DIRECTION('ref_axis',(-0.894427190999916,0.,-0.447213595499958));
#4625=DIRECTION('center_axis',(0.894427190999916,0.,-0.447213595499957));
#4626=DIRECTION('ref_axis',(-0.447213595499957,0.,-0.894427190999916));
#4627=DIRECTION('center_axis',(0.,1.,0.));
#4628=DIRECTION('ref_axis',(0.,0.,1.));
#4629=DIRECTION('center_axis',(0.,-1.,0.));
#4630=DIRECTION('ref_axis',(-0.870367380373861,0.,0.492402907364633));
#4631=DIRECTION('center_axis',(0.,0.,1.));
#4632=DIRECTION('ref_axis',(0.,1.,0.));
#4633=DIRECTION('center_axis',(0.,1.,0.));
#4634=DIRECTION('ref_axis',(-0.870367380373861,0.,0.492402907364633));
#4635=DIRECTION('center_axis',(0.,0.,1.));
#4636=DIRECTION('ref_axis',(-0.707106781186547,0.707106781186547,0.));
#4637=DIRECTION('center_axis',(0.,0.,1.));
#4638=DIRECTION('ref_axis',(0.,1.,0.));
#4639=DIRECTION('',(0.,0.,-1.));
#4640=DIRECTION('center_axis',(-1.,0.,0.));
#4641=DIRECTION('ref_axis',(0.,0.,1.));
#4642=DIRECTION('center_axis',(1.,0.,0.));
#4643=DIRECTION('ref_axis',(0.,-1.,0.));
#4644=DIRECTION('center_axis',(0.,0.,1.));
#4645=DIRECTION('ref_axis',(-0.672021505032249,-0.740531631177353,0.));
#4646=DIRECTION('',(0.,0.,-1.));
#4647=DIRECTION('center_axis',(0.,0.,-1.));
#4648=DIRECTION('ref_axis',(-0.672021505032249,-0.740531631177353,0.));
#4649=DIRECTION('',(0.,0.,1.));
#4650=DIRECTION('center_axis',(0.,0.,1.));
#4651=DIRECTION('ref_axis',(1.,0.,0.));
#4652=DIRECTION('',(-1.,0.,0.));
#4653=DIRECTION('center_axis',(0.,0.,-1.));
#4654=DIRECTION('ref_axis',(1.,0.,0.));
#4655=DIRECTION('center_axis',(-1.,0.,0.));
#4656=DIRECTION('ref_axis',(0.,-0.707106781186547,-0.707106781186548));
#4657=DIRECTION('',(1.,0.,0.));
#4658=DIRECTION('center_axis',(0.,1.,0.));
#4659=DIRECTION('ref_axis',(1.,0.,0.));
#4660=DIRECTION('',(1.,0.,0.));
#4661=DIRECTION('',(0.,0.,1.));
#4662=DIRECTION('',(-0.999957135616594,0.,-0.0092588838126317));
#4663=DIRECTION('',(-0.00925888381263175,0.,0.999957135616594));
#4664=DIRECTION('',(1.,0.,0.));
#4665=DIRECTION('',(0.,0.,1.));
#4666=DIRECTION('',(-1.,0.,0.));
#4667=DIRECTION('center_axis',(0.,-1.,0.));
#4668=DIRECTION('ref_axis',(0.,0.,-1.));
#4669=DIRECTION('center_axis',(0.,-1.,0.));
#4670=DIRECTION('ref_axis',(-0.870367380373861,0.,0.492402907364633));
#4671=DIRECTION('center_axis',(0.,0.,1.));
#4672=DIRECTION('ref_axis',(-1.,0.,0.));
#4673=DIRECTION('center_axis',(0.,1.,0.));
#4674=DIRECTION('ref_axis',(-0.870367380373861,0.,0.492402907364633));
#4675=DIRECTION('center_axis',(0.,0.,-1.));
#4676=DIRECTION('ref_axis',(-0.707106781186547,-0.707106781186547,0.));
#4677=DIRECTION('center_axis',(0.,0.,1.));
#4678=DIRECTION('ref_axis',(-1.,0.,0.));
#4679=DIRECTION('',(0.,0.,1.));
#4680=DIRECTION('center_axis',(-0.119999999999999,0.992773891679269,-6.66133814775086E-17));
#4681=DIRECTION('ref_axis',(-0.992773891679269,-0.119999999999999,0.));
#4682=DIRECTION('center_axis',(2.30755522366023E-14,-0.866025403784422,
-0.500000000000028));
#4683=DIRECTION('ref_axis',(-9.25185853854298E-16,-0.500000000000028,0.866025403784422));
#4684=DIRECTION('center_axis',(0.,0.,1.));
#4685=DIRECTION('ref_axis',(1.,0.,0.));
#4686=DIRECTION('center_axis',(-0.12,-0.992773891679269,0.));
#4687=DIRECTION('ref_axis',(0.992773891679269,-0.12,0.));
#4688=DIRECTION('center_axis',(0.,0.,-1.));
#4689=DIRECTION('ref_axis',(1.58603289232165E-16,-1.,0.));
#4690=DIRECTION('center_axis',(0.,0.,1.));
#4691=DIRECTION('ref_axis',(1.58603289232165E-16,-1.,0.));
#4692=DIRECTION('center_axis',(-0.0963241948601912,-0.990678201521095,-0.0963241948601911));
#4693=DIRECTION('ref_axis',(0.995306362615581,-0.096774193548388,-3.70074341541719E-16));
#4694=DIRECTION('center_axis',(0.894427190999916,0.,-0.447213595499957));
#4695=DIRECTION('ref_axis',(-0.447213595499957,0.,-0.894427190999916));
#4696=DIRECTION('center_axis',(-0.447213595499958,0.,0.894427190999916));
#4697=DIRECTION('ref_axis',(-0.894427190999916,0.,-0.447213595499958));
#4698=DIRECTION('center_axis',(-1.,0.,0.));
#4699=DIRECTION('ref_axis',(0.,0.,1.));
#4700=DIRECTION('center_axis',(1.,0.,0.));
#4701=DIRECTION('ref_axis',(0.,1.,0.));
#4702=DIRECTION('center_axis',(0.,0.,1.));
#4703=DIRECTION('ref_axis',(1.,0.,0.));
#4704=DIRECTION('',(1.,0.,0.));
#4705=DIRECTION('center_axis',(0.,0.,-1.));
#4706=DIRECTION('ref_axis',(1.,0.,0.));
#4707=DIRECTION('center_axis',(0.,0.,-1.));
#4708=DIRECTION('ref_axis',(-0.67202150503225,0.740531631177352,0.));
#4709=DIRECTION('',(0.,0.,-1.));
#4710=DIRECTION('',(0.,0.,1.));
#4711=DIRECTION('center_axis',(0.,0.,1.));
#4712=DIRECTION('ref_axis',(-1.,0.,0.));
#4713=DIRECTION('center_axis',(-0.0963241948601892,-0.990678201521096,0.0963241948601895));
#4714=DIRECTION('ref_axis',(0.,0.0967741935483863,0.995306362615581));
#4715=DIRECTION('center_axis',(-0.894427190999916,0.,-0.447213595499959));
#4716=DIRECTION('ref_axis',(0.447213595499958,0.,-0.894427190999916));
#4717=DIRECTION('center_axis',(0.447213595499958,0.,0.894427190999916));
#4718=DIRECTION('ref_axis',(0.894427190999916,0.,-0.447213595499958));
#4719=DIRECTION('center_axis',(-0.119999999999994,-0.992773891679269,-4.40880173115618E-15));
#4720=DIRECTION('ref_axis',(0.,-4.44089209850062E-15,1.));
#4721=DIRECTION('center_axis',(0.,0.,1.));
#4722=DIRECTION('ref_axis',(1.,0.,0.));
#4723=DIRECTION('center_axis',(-0.12,0.992773891679269,0.));
#4724=DIRECTION('ref_axis',(0.,0.,1.));
#4725=DIRECTION('center_axis',(0.,0.,1.));
#4726=DIRECTION('ref_axis',(0.0536486895476169,0.998559872070685,0.));
#4727=DIRECTION('center_axis',(0.,0.,-1.));
#4728=DIRECTION('ref_axis',(0.0536486895476169,0.998559872070685,0.));
#4729=DIRECTION('center_axis',(0.,0.,1.));
#4730=DIRECTION('ref_axis',(1.,0.,0.));
#4731=DIRECTION('',(0.,0.,1.));
#4732=DIRECTION('center_axis',(0.,0.,1.));
#4733=DIRECTION('ref_axis',(1.,0.,0.));
#4734=DIRECTION('',(0.,0.,-1.));
#4735=DIRECTION('center_axis',(0.,-1.,0.));
#4736=DIRECTION('ref_axis',(1.,0.,0.));
#4737=DIRECTION('',(-1.,0.,0.));
#4738=DIRECTION('',(0.00925888381263175,0.,-0.999957135616594));
#4739=DIRECTION('center_axis',(0.,0.,1.));
#4740=DIRECTION('ref_axis',(1.,0.,0.));
#4741=DIRECTION('center_axis',(-0.999828575531215,0.,-0.0185153868774323));
#4742=DIRECTION('ref_axis',(0.0185153868774323,0.,-0.999828575531215));
#4743=DIRECTION('center_axis',(-0.0092588838126328,-2.96046782826604E-15,
0.999957135616594));
#4744=DIRECTION('ref_axis',(0.999957135616594,0.,0.0092588838126328));
#4745=DIRECTION('center_axis',(0.999957135616594,0.,0.00925888381263175));
#4746=DIRECTION('ref_axis',(0.00925888381263175,3.70058478533254E-16,-0.999957135616594));
#4747=DIRECTION('center_axis',(0.,0.,1.));
#4748=DIRECTION('ref_axis',(1.,0.,0.));
#4749=DIRECTION('center_axis',(0.12,-0.992773891679269,7.10542735760099E-16));
#4750=DIRECTION('ref_axis',(-5.9211894646675E-15,0.,1.));
#4751=DIRECTION('center_axis',(0.,0.,1.));
#4752=DIRECTION('ref_axis',(0.0536486895476169,-0.998559872070685,0.));
#4753=DIRECTION('center_axis',(-0.12,-0.992773891679269,0.));
#4754=DIRECTION('ref_axis',(0.992773891679269,-0.12,0.));
#4755=DIRECTION('center_axis',(0.,0.,-1.));
#4756=DIRECTION('ref_axis',(0.0536486895476169,-0.998559872070685,0.));
#4757=DIRECTION('center_axis',(0.0963241948601898,-0.990678201521096,-0.0963241948601867));
#4758=DIRECTION('ref_axis',(0.,-0.0967741935483834,0.995306362615582));
#4759=DIRECTION('center_axis',(0.447213595499958,0.,0.894427190999916));
#4760=DIRECTION('ref_axis',(0.894427190999916,0.,-0.447213595499958));
#4761=DIRECTION('center_axis',(-0.894427190999916,0.,-0.447213595499959));
#4762=DIRECTION('ref_axis',(0.447213595499959,0.,-0.894427190999916));
#4763=DIRECTION('center_axis',(0.,0.,1.));
#4764=DIRECTION('ref_axis',(0.67202150503225,0.740531631177352,0.));
#4765=DIRECTION('',(0.,0.,-1.));
#4766=DIRECTION('',(0.,0.,1.));
#4767=DIRECTION('center_axis',(1.,0.,0.));
#4768=DIRECTION('ref_axis',(0.,0.707106781186547,-0.707106781186548));
#4769=DIRECTION('',(1.,0.,0.));
#4770=DIRECTION('center_axis',(-0.999828575531215,0.,-0.0185153868774323));
#4771=DIRECTION('ref_axis',(0.0185153868774323,0.,-0.999828575531215));
#4772=DIRECTION('',(-1.,0.,0.));
#4773=DIRECTION('center_axis',(0.,0.,1.));
#4774=DIRECTION('ref_axis',(1.,0.,0.));
#4775=DIRECTION('',(-1.,0.,0.));
#4776=DIRECTION('center_axis',(0.,0.,1.));
#4777=DIRECTION('ref_axis',(1.,0.,0.));
#4778=DIRECTION('center_axis',(0.,0.,-1.));
#4779=DIRECTION('ref_axis',(1.,0.,0.));
#4780=DIRECTION('center_axis',(0.999957135616594,0.,0.00925888381263175));
#4781=DIRECTION('ref_axis',(0.00925888381263175,-3.70058478533254E-16,-0.999957135616594));
#4782=DIRECTION('center_axis',(-0.0092588838126328,2.96046782826604E-15,
0.999957135616594));
#4783=DIRECTION('ref_axis',(0.,-1.,2.96059473233375E-15));
#4784=DIRECTION('center_axis',(-0.00925888381263175,0.,0.999957135616594));
#4785=DIRECTION('ref_axis',(0.707076471490368,-0.70710678118655,0.00654701953012897));
#4786=DIRECTION('',(-0.00925888381263175,0.,0.999957135616594));
#4787=DIRECTION('center_axis',(0.0092588838126328,0.,-0.999957135616594));
#4788=DIRECTION('ref_axis',(0.999957135616594,0.,0.0092588838126328));
#4789=DIRECTION('',(0.00925888381263175,0.,-0.999957135616594));
#4790=DIRECTION('center_axis',(-0.999957135616594,0.,-0.00925888381263175));
#4791=DIRECTION('ref_axis',(-0.00925888381263226,0.,0.999957135616594));
#4792=DIRECTION('center_axis',(0.999957135616594,0.,0.00925888381263175));
#4793=DIRECTION('ref_axis',(0.00886470634978,-0.288675134594812,-0.957386068233709));
#4794=DIRECTION('center_axis',(1.37059013214855E-17,-1.,-1.48023391413303E-15));
#4795=DIRECTION('ref_axis',(0.999957135616594,0.,0.0092588838126328));
#4796=DIRECTION('center_axis',(-0.999957135616594,0.,-0.00925888381263175));
#4797=DIRECTION('ref_axis',(0.00886470634977989,-0.288675134594812,-0.957386068233709));
#4798=DIRECTION('center_axis',(0.,-1.,0.));
#4799=DIRECTION('ref_axis',(0.700529451960246,0.,0.713623491020495));
#4800=DIRECTION('center_axis',(0.,-1.,0.));
#4801=DIRECTION('ref_axis',(0.999957135616594,0.,0.00925888381263269));
#4802=DIRECTION('',(0.,-1.,0.));
#4803=DIRECTION('',(0.,1.,0.));
#4804=DIRECTION('center_axis',(-0.999989286143139,2.19273273023019E-16,
0.00462899545630677));
#4805=DIRECTION('ref_axis',(-0.00462899545630677,-4.66248702327598E-14,
-0.999989286143139));
#4806=DIRECTION('center_axis',(2.89281217569941E-15,0.212757250200078,-0.977105087739953));
#4807=DIRECTION('ref_axis',(-0.0019699752792827,0.977103191762131,0.212756837365233));
#4808=DIRECTION('center_axis',(1.,0.,0.));
#4809=DIRECTION('ref_axis',(0.,-4.69665885671789E-14,-1.));
#4810=DIRECTION('center_axis',(0.,0.212757250200078,0.977105087739953));
#4811=DIRECTION('ref_axis',(-0.0019699752792827,-0.977103191762131,0.212756837365232));
#4812=DIRECTION('center_axis',(-1.,0.,0.));
#4813=DIRECTION('ref_axis',(0.,-1.76594458083507E-13,1.));
#4814=DIRECTION('center_axis',(0.999998740412341,-2.80330577459927E-16,
0.00158719051532392));
#4815=DIRECTION('ref_axis',(-0.00158719051532392,-1.7659683092229E-13,0.999998740412341));
#4816=DIRECTION('center_axis',(1.,0.,0.));
#4817=DIRECTION('ref_axis',(0.,-1.48023391413302E-15,-1.));
#4818=DIRECTION('center_axis',(-0.999989286143139,6.85228978196936E-18,
0.00462899545630677));
#4819=DIRECTION('ref_axis',(-0.00462899545630677,-1.4801546105638E-15,-0.999989286143139));
#4820=DIRECTION('center_axis',(-0.999957135616594,0.,-0.00925888381263175));
#4821=DIRECTION('ref_axis',(-0.00925888381263226,0.,0.999957135616594));
#4822=DIRECTION('center_axis',(-0.999957135616594,0.,-0.00925888381263175));
#4823=DIRECTION('ref_axis',(0.0088647063497799,0.288675134594811,-0.957386068233709));
#4824=DIRECTION('center_axis',(1.37059013214855E-17,1.,-1.48023391413302E-15));
#4825=DIRECTION('ref_axis',(-0.00925888381264173,1.48029736616688E-15,0.999957135616594));
#4826=DIRECTION('center_axis',(0.999957135616594,0.,0.00925888381263175));
#4827=DIRECTION('ref_axis',(0.00886470634978,0.288675134594811,-0.957386068233709));
#4828=DIRECTION('center_axis',(0.,-1.,0.));
#4829=DIRECTION('ref_axis',(0.700529451960246,0.,0.713623491020495));
#4830=DIRECTION('center_axis',(0.,1.,0.));
#4831=DIRECTION('ref_axis',(-0.00925888381262989,0.,0.999957135616594));
#4832=DIRECTION('',(0.,1.,0.));
#4833=DIRECTION('',(0.,-1.,0.));
#4834=DIRECTION('center_axis',(0.00925888381263175,0.,-0.999957135616594));
#4835=DIRECTION('ref_axis',(0.707076471490368,0.70710678118655,0.00654701953012897));
#4836=DIRECTION('center_axis',(0.0092588838126328,0.,-0.999957135616594));
#4837=DIRECTION('ref_axis',(0.,1.,0.));
#4838=DIRECTION('',(0.00925888381263175,0.,-0.999957135616594));
#4839=DIRECTION('center_axis',(0.404450867664508,-0.816496580927731,0.412010714640715));
#4840=DIRECTION('ref_axis',(0.571979902364718,0.577350269189621,0.582671140487942));
#4841=DIRECTION('center_axis',(0.999957135616594,0.,0.0092588838126317));
#4842=DIRECTION('ref_axis',(-0.00654701953012685,0.707106781186547,0.70707647149037));
#4843=DIRECTION('center_axis',(-0.404450867664508,-0.816496580927731,-0.412010714640715));
#4844=DIRECTION('ref_axis',(0.571979902364718,-0.577350269189621,0.582671140487942));
#4845=DIRECTION('center_axis',(0.999957135616594,0.,0.0092588838126317));
#4846=DIRECTION('ref_axis',(-0.00654701953012685,-0.707106781186547,0.70707647149037));
#4847=DIRECTION('center_axis',(0.,0.,1.));
#4848=DIRECTION('ref_axis',(-1.,0.,0.));
#4849=DIRECTION('',(0.,0.,1.));
#4850=DIRECTION('center_axis',(0.,1.,0.));
#4851=DIRECTION('ref_axis',(1.,0.,0.));
#4852=DIRECTION('',(-1.,0.,0.));
#4853=DIRECTION('',(0.999957135616594,0.,0.0092588838126317));
#4854=DIRECTION('',(0.,0.,-1.));
#4855=DIRECTION('',(-1.,0.,0.));
#4856=DIRECTION('',(-1.,0.,0.));
#4857=DIRECTION('center_axis',(-0.999957135616594,0.,-0.0092588838126317));
#4858=DIRECTION('ref_axis',(-0.00654701953012895,-0.707106781186548,0.70707647149037));
#4859=DIRECTION('',(-0.999957135616594,0.,-0.0092588838126317));
#4860=DIRECTION('center_axis',(1.,0.,0.));
#4861=DIRECTION('ref_axis',(0.,-8.99427132075075E-13,1.));
#4862=DIRECTION('center_axis',(0.0092588838126317,0.,-0.999957135616594));
#4863=DIRECTION('ref_axis',(0.,-1.,0.));
#4864=DIRECTION('',(0.999957135616594,0.,0.00925888381263174));
#4865=DIRECTION('',(0.,1.,0.));
#4866=DIRECTION('center_axis',(-0.999957135616594,0.,-0.0092588838126317));
#4867=DIRECTION('ref_axis',(0.0092588838126317,-1.48029736616688E-15,-0.999957135616594));
#4868=DIRECTION('',(0.999957135616594,0.,0.00925888381263174));
#4869=DIRECTION('center_axis',(1.,0.,0.));
#4870=DIRECTION('ref_axis',(0.,-1.48023391413302E-15,-1.));
#4871=DIRECTION('center_axis',(-0.999957135616594,0.,-0.0092588838126317));
#4872=DIRECTION('ref_axis',(-0.00196997527928334,0.97710319176213,0.212756837365233));
#4873=DIRECTION('',(0.999957135616594,0.,0.00925888381263174));
#4874=DIRECTION('center_axis',(-1.,0.,0.));
#4875=DIRECTION('ref_axis',(0.,-1.55456280282127E-13,1.));
#4876=DIRECTION('center_axis',(-0.999957135616594,0.,-0.0092588838126317));
#4877=DIRECTION('ref_axis',(0.00196997527928333,-0.977103191762131,-0.212756837365232));
#4878=DIRECTION('',(0.999957135616594,0.,0.00925888381263174));
#4879=DIRECTION('center_axis',(1.,0.,0.));
#4880=DIRECTION('ref_axis',(0.,-3.29791490337855E-13,-1.));
#4881=DIRECTION('center_axis',(0.0092588838126317,0.,-0.999957135616594));
#4882=DIRECTION('ref_axis',(0.,-1.,0.));
#4883=DIRECTION('',(0.999957135616594,0.,0.0092588838126317));
#4884=DIRECTION('',(0.,1.,0.));
#4885=DIRECTION('center_axis',(0.999957135616594,0.,0.0092588838126317));
#4886=DIRECTION('ref_axis',(-0.00654701953012895,0.707106781186548,0.70707647149037));
#4887=DIRECTION('center_axis',(1.,0.,0.));
#4888=DIRECTION('ref_axis',(0.,8.99427132075075E-13,1.));
#4889=DIRECTION('center_axis',(-1.,0.,0.));
#4890=DIRECTION('ref_axis',(0.,0.,1.));
#4891=DIRECTION('',(0.,1.,0.));
#4892=DIRECTION('center_axis',(1.,0.,0.));
#4893=DIRECTION('ref_axis',(0.,1.,0.));
#4894=DIRECTION('center_axis',(-1.,0.,0.));
#4895=DIRECTION('ref_axis',(0.,1.,0.));
#4896=DIRECTION('center_axis',(-0.999957135616594,0.,-0.00925888381263175));
#4897=DIRECTION('ref_axis',(0.00925888381263175,0.,-0.999957135616594));
#4898=DIRECTION('center_axis',(-1.,0.,0.));
#4899=DIRECTION('ref_axis',(0.,1.,0.));
#4900=DIRECTION('',(-1.,0.,0.));
#4901=DIRECTION('center_axis',(1.,0.,0.));
#4902=DIRECTION('ref_axis',(0.,0.,-1.));
#4903=DIRECTION('',(0.,1.,0.));
#4904=DIRECTION('',(0.,1.,0.));
#4905=DIRECTION('center_axis',(0.,0.,-1.));
#4906=DIRECTION('ref_axis',(0.67202150503225,-0.740531631177352,0.));
#4907=DIRECTION('center_axis',(0.,0.,-1.));
#4908=DIRECTION('ref_axis',(0.67202150503225,-0.740531631177352,0.));
#4909=DIRECTION('center_axis',(-1.,0.,0.));
#4910=DIRECTION('ref_axis',(0.,-0.707106781186547,-0.707106781186548));
#4911=DIRECTION('',(-1.,0.,0.));
#4912=DIRECTION('center_axis',(0.,0.,1.));
#4913=DIRECTION('ref_axis',(1.,0.,0.));
#4914=DIRECTION('center_axis',(0.,0.,-1.));
#4915=DIRECTION('ref_axis',(1.,0.,0.));
#4916=DIRECTION('center_axis',(1.,0.,0.));
#4917=DIRECTION('ref_axis',(0.,0.707106781186547,-0.707106781186548));
#4918=DIRECTION('center_axis',(0.,0.,1.));
#4919=DIRECTION('ref_axis',(1.,0.,0.));
#4920=DIRECTION('',(0.,0.,-1.));
#4921=DIRECTION('center_axis',(0.,0.,-1.));
#4922=DIRECTION('ref_axis',(1.,0.,0.));
#4923=DIRECTION('center_axis',(0.,0.,1.));
#4924=DIRECTION('ref_axis',(1.,0.,0.));
#4925=DIRECTION('center_axis',(0.,0.,1.));
#4926=DIRECTION('ref_axis',(1.,0.,0.));
#4927=DIRECTION('center_axis',(0.,0.,1.));
#4928=DIRECTION('ref_axis',(1.,0.,0.));
#4929=DIRECTION('',(0.,0.,-1.));
#4930=DIRECTION('center_axis',(0.,0.,1.));
#4931=DIRECTION('ref_axis',(1.,0.,0.));
#4932=DIRECTION('',(0.,0.,-1.));
#4933=DIRECTION('center_axis',(0.,0.,-1.));
#4934=DIRECTION('ref_axis',(1.,0.,0.));
#4935=DIRECTION('center_axis',(0.,0.,1.));
#4936=DIRECTION('ref_axis',(1.,0.,0.));
#4937=DIRECTION('',(0.,0.,-1.));
#4938=DIRECTION('center_axis',(0.,1.,0.));
#4939=DIRECTION('ref_axis',(-1.,0.,0.));
#4940=DIRECTION('',(-0.00925888381263175,0.,0.999957135616594));
#4941=DIRECTION('center_axis',(1.,0.,0.));
#4942=DIRECTION('ref_axis',(0.,1.,0.));
#4943=DIRECTION('center_axis',(-1.,0.,0.));
#4944=DIRECTION('ref_axis',(0.,1.,0.));
#4945=DIRECTION('',(-0.866025403784439,0.5,-6.12323399573677E-17));
#4946=DIRECTION('center_axis',(-1.,0.,0.));
#4947=DIRECTION('ref_axis',(0.,1.,0.));
#4948=DIRECTION('',(-1.,0.,0.));
#4949=DIRECTION('center_axis',(1.,0.,0.));
#4950=DIRECTION('ref_axis',(0.,1.,0.));
#4951=DIRECTION('center_axis',(-1.,0.,0.));
#4952=DIRECTION('ref_axis',(0.,1.,0.));
#4953=DIRECTION('',(-0.866025403784439,0.5,-6.12323399573677E-17));
#4954=DIRECTION('center_axis',(-1.,0.,0.));
#4955=DIRECTION('ref_axis',(0.,1.,0.));
#4956=DIRECTION('',(-1.,0.,0.));
#4957=DIRECTION('center_axis',(0.,0.,1.));
#4958=DIRECTION('ref_axis',(1.,0.,0.));
#4959=DIRECTION('center_axis',(0.,0.,1.));
#4960=DIRECTION('ref_axis',(1.,0.,0.));
#4961=DIRECTION('',(0.,1.,0.));
#4962=DIRECTION('center_axis',(0.,1.,0.));
#4963=DIRECTION('ref_axis',(-1.,0.,5.07530525542928E-16));
#4964=DIRECTION('center_axis',(0.,0.,-1.));
#4965=DIRECTION('ref_axis',(-1.,0.,0.));
#4966=DIRECTION('',(0.,1.,0.));
#4967=DIRECTION('center_axis',(0.999957135616594,0.,0.00925888381263175));
#4968=DIRECTION('ref_axis',(0.00925888381263175,0.,-0.999957135616594));
#5607=CARTESIAN_POINT('',(0.,0.,0.));
#5608=CARTESIAN_POINT('Origin',(183.750010137059,-16.,26.9988426616481));
#5609=CARTESIAN_POINT('',(0.,-12.5,25.2974497380605));
#5610=CARTESIAN_POINT('',(0.,-16.,25.2974497380605));
#5611=CARTESIAN_POINT('',(0.,-8.,25.2974497380605));
#5612=CARTESIAN_POINT('',(183.750010137059,-12.5,26.9988426616481));
#5613=CARTESIAN_POINT('',(183.750010137059,-12.5,26.9988426616481));
#5614=CARTESIAN_POINT('',(183.750010137059,-16.,26.9988426616481));
#5615=CARTESIAN_POINT('',(183.750010137059,-8.,26.9988426616481));
#5616=CARTESIAN_POINT('',(183.750010137059,-16.,26.9988426616481));
#5617=CARTESIAN_POINT('Origin',(184.,-16.,0.));
#5618=CARTESIAN_POINT('',(0.,-16.,0.));
#5619=CARTESIAN_POINT('',(0.,-16.,0.));
#5620=CARTESIAN_POINT('',(184.,-16.,8.32667268468867E-16));
#5621=CARTESIAN_POINT('',(183.73612181134,-16.,28.4987783650729));
#5622=CARTESIAN_POINT('',(184.,-16.,0.));
#5623=CARTESIAN_POINT('Origin',(183.750010137059,16.,26.9988426616481));
#5624=CARTESIAN_POINT('',(184.,16.,8.32667268468867E-16));
#5625=CARTESIAN_POINT('',(0.,16.,0.));
#5626=CARTESIAN_POINT('',(183.87500506853,16.,0.));
#5627=CARTESIAN_POINT('',(183.750010137059,16.,26.9988426616481));
#5628=CARTESIAN_POINT('',(183.611126879869,16.,41.998199695897));
#5629=CARTESIAN_POINT('',(0.,16.,25.2974497380605));
#5630=CARTESIAN_POINT('',(183.750010137059,16.,26.9988426616481));
#5631=CARTESIAN_POINT('',(0.,16.,13.499421330824));
#5632=CARTESIAN_POINT('Origin',(183.601867996057,-12.5,42.9981568315136));
#5633=CARTESIAN_POINT('',(158.47224362268,12.5,42.7654745854044));
#5634=CARTESIAN_POINT('',(158.47224362268,-12.5,42.7654745854044));
#5635=CARTESIAN_POINT('',(158.47224362268,-6.25,42.7654745854044));
#5636=CARTESIAN_POINT('',(183.601867996057,12.5,42.9981568315136));
#5637=CARTESIAN_POINT('',(183.601867996057,12.5,42.9981568315136));
#5638=CARTESIAN_POINT('',(183.601867996057,-12.5,42.9981568315136));
#5639=CARTESIAN_POINT('',(183.601867996057,-6.25,42.9981568315136));
#5640=CARTESIAN_POINT('',(183.601867996057,-12.5,42.9981568315136));
#5641=CARTESIAN_POINT('Origin',(183.750010137059,-12.5,26.9988426616481));
#5642=CARTESIAN_POINT('',(0.,-12.5,41.298135597594));
#5643=CARTESIAN_POINT('',(0.,-12.5,13.499421330824));
#5644=CARTESIAN_POINT('',(31.47224362268,-12.5,41.5895459357437));
#5645=CARTESIAN_POINT('',(183.601867996057,-12.5,42.9981568315136));
#5646=CARTESIAN_POINT('',(31.47224362268,-12.5,37.));
#5647=CARTESIAN_POINT('',(31.47224362268,-12.5,54.499421330824));
#5648=CARTESIAN_POINT('',(158.47224362268,-12.5,37.));
#5649=CARTESIAN_POINT('',(107.61112687987,-12.5,37.));
#5650=CARTESIAN_POINT('',(158.47224362268,-12.5,31.999421330824));
#5651=CARTESIAN_POINT('',(183.611126879869,-12.5,41.998199695897));
#5652=CARTESIAN_POINT('Origin',(183.750010137059,12.5,26.9988426616481));
#5653=CARTESIAN_POINT('',(0.,12.5,25.2974497380605));
#5654=CARTESIAN_POINT('',(0.,6.25,25.2974497380605));
#5655=CARTESIAN_POINT('',(183.750010137059,12.5,26.9988426616481));
#5656=CARTESIAN_POINT('',(183.750010137059,6.25,26.9988426616481));
#5657=CARTESIAN_POINT('',(183.750010137059,12.5,26.9988426616481));
#5658=CARTESIAN_POINT('Origin',(183.601867996057,12.5,42.9981568315136));
#5659=CARTESIAN_POINT('',(0.,12.5,41.298135597594));
#5660=CARTESIAN_POINT('',(0.,12.5,21.4990784157568));
#5661=CARTESIAN_POINT('',(183.537055809368,12.5,49.9978567808297));
#5662=CARTESIAN_POINT('',(158.47224362268,12.5,37.));
#5663=CARTESIAN_POINT('',(158.47224362268,12.5,39.9990784157568));
#5664=CARTESIAN_POINT('',(31.47224362268,12.5,37.));
#5665=CARTESIAN_POINT('',(107.537055809368,12.5,37.));
#5666=CARTESIAN_POINT('',(31.47224362268,12.5,41.5895459357437));
#5667=CARTESIAN_POINT('',(31.47224362268,12.5,62.4990784157568));
#5668=CARTESIAN_POINT('',(183.601867996057,12.5,42.9981568315136));
#5669=CARTESIAN_POINT('Origin',(183.601867996057,-12.5,42.9981568315136));
#5670=CARTESIAN_POINT('',(0.,-6.25,41.2981355975939));
#5671=CARTESIAN_POINT('',(31.47224362268,-6.25,41.5895459357437));
#5672=CARTESIAN_POINT('Origin',(31.47224362268,0.,82.));
#5673=CARTESIAN_POINT('',(31.47224362268,35.,37.));
#5674=CARTESIAN_POINT('',(31.47224362268,0.,37.));
#5675=CARTESIAN_POINT('',(31.47224362268,35.,82.));
#5676=CARTESIAN_POINT('',(31.47224362268,35.,37.));
#5677=CARTESIAN_POINT('',(31.47224362268,-35.,82.));
#5678=CARTESIAN_POINT('',(31.47224362268,0.,82.));
#5679=CARTESIAN_POINT('',(31.47224362268,-35.,37.));
#5680=CARTESIAN_POINT('',(31.47224362268,-35.,37.));
#5681=CARTESIAN_POINT('',(31.47224362268,0.,37.));
#5682=CARTESIAN_POINT('',(31.47224362268,-22.,62.));
#5683=CARTESIAN_POINT('Origin',(31.47224362268,-19.,62.));
#5684=CARTESIAN_POINT('',(31.47224362268,16.,62.));
#5685=CARTESIAN_POINT('Origin',(31.47224362268,19.,62.));
#5686=CARTESIAN_POINT('Origin',(31.47224362268,0.,37.));
#5687=CARTESIAN_POINT('',(158.47224362268,35.,37.));
#5688=CARTESIAN_POINT('',(158.47224362268,0.,37.));
#5689=CARTESIAN_POINT('',(158.47224362268,35.,37.));
#5690=CARTESIAN_POINT('Origin',(0.,0.,0.));
#5691=CARTESIAN_POINT('',(0.,-35.,0.));
#5692=CARTESIAN_POINT('',(0.,0.,0.));
#5693=CARTESIAN_POINT('',(5.35595873207839E-16,-34.9999999999999,5.80384757729347));
#5694=CARTESIAN_POINT('',(0.,-35.,0.));
#5695=CARTESIAN_POINT('',(0.,-32.,11.));
#5696=CARTESIAN_POINT('Origin',(0.,-38.,11.));
#5697=CARTESIAN_POINT('',(0.,-32.,52.));
#5698=CARTESIAN_POINT('',(0.,-32.,20.5));
#5699=CARTESIAN_POINT('',(0.,32.,52.));
#5700=CARTESIAN_POINT('',(0.,0.,52.));
#5701=CARTESIAN_POINT('',(0.,32.,11.));
#5702=CARTESIAN_POINT('',(0.,32.,20.5));
#5703=CARTESIAN_POINT('',(-1.88109076926235E-16,34.9999999999997,5.80384757729367));
#5704=CARTESIAN_POINT('Origin',(0.,38.,11.));
#5705=CARTESIAN_POINT('',(0.,35.,0.));
#5706=CARTESIAN_POINT('',(0.,35.,0.));
#5707=CARTESIAN_POINT('',(0.,0.,0.));
#5708=CARTESIAN_POINT('Origin',(184.,0.,0.));
#5709=CARTESIAN_POINT('',(184.,-35.,0.));
#5710=CARTESIAN_POINT('',(184.,0.,0.));
#5711=CARTESIAN_POINT('',(128.131421846764,-37.7096774193548,0.));
#5712=CARTESIAN_POINT('Origin',(156.,-35.,0.));
#5713=CARTESIAN_POINT('',(125.145502758917,-35.,0.));
#5714=CARTESIAN_POINT('Origin',(125.145502758917,-38.,0.));
#5715=CARTESIAN_POINT('',(58.854497241083,-35.,0.));
#5716=CARTESIAN_POINT('',(0.,-35.,0.));
#5717=CARTESIAN_POINT('',(55.8685781532363,-37.7096774193548,0.));
#5718=CARTESIAN_POINT('Origin',(58.854497241083,-38.,0.));
#5719=CARTESIAN_POINT('Origin',(28.,-35.,0.));
#5720=CARTESIAN_POINT('',(24.,-50.,0.));
#5721=CARTESIAN_POINT('Origin',(28.,-50.,0.));
#5722=CARTESIAN_POINT('',(152.,-50.,0.));
#5723=CARTESIAN_POINT('Origin',(156.,-50.,0.));
#5724=CARTESIAN_POINT('Ctrl Pts',(3.,36.4999999999997,8.40192378864683));
#5725=CARTESIAN_POINT('Ctrl Pts',(2.99999999999998,36.954480338638,8.13952944279256));
#5726=CARTESIAN_POINT('Ctrl Pts',(3.05470342200826,37.4790034882233,8.));
#5727=CARTESIAN_POINT('Ctrl Pts',(3.18065270801829,38.,8.));
#5728=CARTESIAN_POINT('Ctrl Pts',(2.10240209897434,36.4999999999997,8.40192378864684));
#5729=CARTESIAN_POINT('Ctrl Pts',(2.11299837157538,36.9775281360311,8.12577095949316));
#5730=CARTESIAN_POINT('Ctrl Pts',(2.17111074773699,37.5492218178523,7.98077045544578));
#5731=CARTESIAN_POINT('Ctrl Pts',(2.28954094665391,38.1077117481231,8.));
#5732=CARTESIAN_POINT('Ctrl Pts',(0.547958039803657,36.1236422123021,7.75005297853055));
#5733=CARTESIAN_POINT('Ctrl Pts',(0.575502703260674,36.7685292312036,7.39913053299978));
#5734=CARTESIAN_POINT('Ctrl Pts',(0.639381985506942,37.5362747159179,7.21746293992274));
#5735=CARTESIAN_POINT('Ctrl Pts',(0.746329468633318,38.2942450352236,7.24728442460496));
#5736=CARTESIAN_POINT('Ctrl Pts',(-5.28707639943152E-15,35.3365992128841,
6.38685451579749));
#5737=CARTESIAN_POINT('Ctrl Pts',(0.0123332119636002,36.2492271656458,5.91410134300127));
#5738=CARTESIAN_POINT('Ctrl Pts',(0.0752933955656041,37.3077055625156,5.66439679042059));
#5739=CARTESIAN_POINT('Ctrl Pts',(0.202331032980483,38.36,5.67319842576924));
#5740=CARTESIAN_POINT('Ctrl Pts',(2.22044604925031E-15,34.9999999999994,
5.80384757729366));
#5741=CARTESIAN_POINT('Ctrl Pts',(-1.91613381295638E-14,36.0180359585492,
5.27905888558515));
#5742=CARTESIAN_POINT('Ctrl Pts',(0.0612678326492503,37.1929678136203,5.));
#5743=CARTESIAN_POINT('Ctrl Pts',(0.202331032980483,38.36,5.));
#5744=CARTESIAN_POINT('',(3.18065270801829,38.,8.));
#5745=CARTESIAN_POINT('',(0.202331032980484,38.36,5.));
#5746=CARTESIAN_POINT('Origin',(3.18065270801829,38.,5.));
#5747=CARTESIAN_POINT('Ctrl Pts',(0.202331032980483,38.36,5.));
#5748=CARTESIAN_POINT('Ctrl Pts',(0.0612678326492503,37.1929678136203,5.));
#5749=CARTESIAN_POINT('Ctrl Pts',(-1.91613381295638E-14,36.0180359585492,
5.27905888558515));
#5750=CARTESIAN_POINT('Ctrl Pts',(2.22044604925031E-15,34.9999999999994,
5.80384757729366));
#5751=CARTESIAN_POINT('',(3.,36.4999999999997,8.40192378864683));
#5752=CARTESIAN_POINT('Origin',(3.,34.9999999999995,5.80384757729367));
#5753=CARTESIAN_POINT('Ctrl Pts',(3.,36.4999999999997,8.40192378864683));
#5754=CARTESIAN_POINT('Ctrl Pts',(2.99999999999998,36.954480338638,8.13952944279256));
#5755=CARTESIAN_POINT('Ctrl Pts',(3.05470342200826,37.4790034882233,8.));
#5756=CARTESIAN_POINT('Ctrl Pts',(3.18065270801829,38.,8.));
#5757=CARTESIAN_POINT('Origin',(28.,35.,5.));
#5758=CARTESIAN_POINT('',(52.8193472919817,38.,8.));
#5759=CARTESIAN_POINT('',(55.7976689670195,38.36,5.));
#5760=CARTESIAN_POINT('Origin',(52.8193472919817,38.,5.));
#5761=CARTESIAN_POINT('Origin',(28.,35.,5.));
#5762=CARTESIAN_POINT('Origin',(28.,35.,8.));
#5763=CARTESIAN_POINT('Ctrl Pts',(55.8685781532363,37.7096774193548,5.02816182430651));
#5764=CARTESIAN_POINT('Ctrl Pts',(55.8475407647763,37.926043434088,5.00937844175291));
#5765=CARTESIAN_POINT('Ctrl Pts',(55.8238771966224,38.1431762825265,5.));
#5766=CARTESIAN_POINT('Ctrl Pts',(55.7976689670195,38.36,5.));
#5767=CARTESIAN_POINT('Ctrl Pts',(55.8602609046479,37.7952189272299,5.91625914580451));
#5768=CARTESIAN_POINT('Ctrl Pts',(55.8413719151341,37.9830850669533,5.90163360405696));
#5769=CARTESIAN_POINT('Ctrl Pts',(55.8203385684754,38.1717572674891,5.89534108170859));
#5770=CARTESIAN_POINT('Ctrl Pts',(55.7976689670195,38.36,5.89759790102565));
#5771=CARTESIAN_POINT('Ctrl Pts',(55.1056560895983,37.8713923378241,7.45429472319515));
#5772=CARTESIAN_POINT('Ctrl Pts',(55.0885194723629,38.0040411687438,7.44665978236163));
#5773=CARTESIAN_POINT('Ctrl Pts',(55.0699339818664,38.1370427186257,7.44582650050821));
#5774=CARTESIAN_POINT('Ctrl Pts',(55.0499325631178,38.2696185252047,7.45169302838196));
#5775=CARTESIAN_POINT('Ctrl Pts',(53.548732056513,37.7738335502611,8.00784297571193));
#5776=CARTESIAN_POINT('Ctrl Pts',(53.5304285848741,37.875964951252,8.00001814579437));
#5777=CARTESIAN_POINT('Ctrl Pts',(53.51008589056,37.978663056326,7.99737324321024));
#5778=CARTESIAN_POINT('Ctrl Pts',(53.487681113005,38.0807838110923,8.));
#5779=CARTESIAN_POINT('Ctrl Pts',(52.8826590653895,37.7096774193548,8.01408091215326));
#5780=CARTESIAN_POINT('Ctrl Pts',(52.8638756828359,37.8062693902182,8.00468922087643));
#5781=CARTESIAN_POINT('Ctrl Pts',(52.8427474969843,37.9032036975564,8.));
#5782=CARTESIAN_POINT('Ctrl Pts',(52.8193472919817,38.,8.));
#5783=CARTESIAN_POINT('',(52.8826590653895,37.7096774193548,8.01408091215326));
#5784=CARTESIAN_POINT('Ctrl Pts',(52.8193472919817,38.,8.));
#5785=CARTESIAN_POINT('Ctrl Pts',(52.8427474969843,37.9032036975564,8.));
#5786=CARTESIAN_POINT('Ctrl Pts',(52.8638756828359,37.8062693902182,8.00468922087643));
#5787=CARTESIAN_POINT('Ctrl Pts',(52.8826590653895,37.7096774193548,8.01408091215326));
#5788=CARTESIAN_POINT('',(55.8685781532363,37.7096774193548,5.02816182430651));
#5789=CARTESIAN_POINT('Origin',(52.8826590653895,37.4193548387097,5.02816182430651));
#5790=CARTESIAN_POINT('Ctrl Pts',(55.8685781532363,37.7096774193548,5.02816182430651));
#5791=CARTESIAN_POINT('Ctrl Pts',(55.8475407647763,37.926043434088,5.00937844175291));
#5792=CARTESIAN_POINT('Ctrl Pts',(55.8238771966224,38.1431762825265,5.));
#5793=CARTESIAN_POINT('Ctrl Pts',(55.7976689670195,38.36,5.));
#5794=CARTESIAN_POINT('Ctrl Pts',(52.8826590653895,37.7096774193548,8.01408091215326));
#5795=CARTESIAN_POINT('Ctrl Pts',(52.9234112434749,37.5001127583042,8.03445700119595));
#5796=CARTESIAN_POINT('Ctrl Pts',(53.1775159289433,36.8777334443635,8.16150934393013));
#5797=CARTESIAN_POINT('Ctrl Pts',(54.243086357739,35.9425957985175,8.69429455832799));
#5798=CARTESIAN_POINT('Ctrl Pts',(56.3283651995436,35.1800659070611,9.73693397923028));
#5799=CARTESIAN_POINT('Ctrl Pts',(58.0122855606517,35.,10.5788941597843));
#5800=CARTESIAN_POINT('Ctrl Pts',(58.854497241083,35.,11.));
#5801=CARTESIAN_POINT('Ctrl Pts',(53.7707563868875,37.7952189272299,8.00576366356483));
#5802=CARTESIAN_POINT('Ctrl Pts',(53.7976964911934,37.6462990978492,8.01387139589604));
#5803=CARTESIAN_POINT('Ctrl Pts',(53.9641832386802,37.1877421817658,8.06350064714943));
#5804=CARTESIAN_POINT('Ctrl Pts',(54.7636697148025,36.2427780971064,8.41333065085001));
#5805=CARTESIAN_POINT('Ctrl Pts',(56.5682125706966,35.2513707994457,9.49453429056375));
#5806=CARTESIAN_POINT('Ctrl Pts',(58.0924961968832,35.,10.4986835235528));
#5807=CARTESIAN_POINT('Ctrl Pts',(58.854497241083,35.,11.));
#5808=CARTESIAN_POINT('Ctrl Pts',(55.3087758987271,37.8713886997517,7.25113749710106));
#5809=CARTESIAN_POINT('Ctrl Pts',(55.3128774402037,37.7745857657828,7.25775185774585));
#5810=CARTESIAN_POINT('Ctrl Pts',(55.332435648546,37.4546465421952,7.29305669671663));
#5811=CARTESIAN_POINT('Ctrl Pts',(55.6785458516857,36.4828390697622,7.69460851516791));
#5812=CARTESIAN_POINT('Ctrl Pts',(56.9905659808484,35.3039288072282,9.07594546731005));
#5813=CARTESIAN_POINT('Ctrl Pts',(58.2328648102884,35.,10.3583149101475));
#5814=CARTESIAN_POINT('Ctrl Pts',(58.854497241083,35.,11.));
#5815=CARTESIAN_POINT('Ctrl Pts',(55.862340216795,37.7738335502611,5.69423481543001));
#5816=CARTESIAN_POINT('Ctrl Pts',(55.8737235797682,37.6091470033402,5.72485515984047));
#5817=CARTESIAN_POINT('Ctrl Pts',(55.9430708156095,37.1082524544471,5.91363113676918));
#5818=CARTESIAN_POINT('Ctrl Pts',(56.339900292733,36.1672073699739,6.78103264850998));
#5819=CARTESIAN_POINT('Ctrl Pts',(57.4107265395028,35.2340992431039,8.6549624533521));
#5820=CARTESIAN_POINT('Ctrl Pts',(58.3732334236937,35.,10.2179462967423));
#5821=CARTESIAN_POINT('Ctrl Pts',(58.854497241083,35.,11.));
#5822=CARTESIAN_POINT('Ctrl Pts',(55.8685781532363,37.7096774193548,5.02816182430651));
#5823=CARTESIAN_POINT('Ctrl Pts',(55.888954242279,37.5001127583042,5.0689140023919));
#5824=CARTESIAN_POINT('Ctrl Pts',(56.0160065850132,36.8777334443635,5.32301868786026));
#5825=CARTESIAN_POINT('Ctrl Pts',(56.548791799411,35.9425957985175,6.38858911665598));
#5826=CARTESIAN_POINT('Ctrl Pts',(57.5914312203133,35.1800659070611,8.47386795846057));
#5827=CARTESIAN_POINT('Ctrl Pts',(58.4333914008674,35.,10.1577883195686));
#5828=CARTESIAN_POINT('Ctrl Pts',(58.854497241083,35.,11.));
#5829=CARTESIAN_POINT('',(58.854497241083,35.,11.));
#5830=CARTESIAN_POINT('Origin',(58.854497241083,38.,11.));
#5831=CARTESIAN_POINT('Origin',(58.854497241083,38.,11.));
#5832=CARTESIAN_POINT('Origin',(35.,32.,52.));
#5833=CARTESIAN_POINT('',(16.97224362268,32.,82.));
#5834=CARTESIAN_POINT('',(23.8644712743399,35.,82.));
#5835=CARTESIAN_POINT('Ctrl Pts',(16.97224362268,32.,82.));
#5836=CARTESIAN_POINT('Ctrl Pts',(16.97224362268,32.1342826532508,82.));
#5837=CARTESIAN_POINT('Ctrl Pts',(16.9946832528106,32.2938517592452,82.));
#5838=CARTESIAN_POINT('Ctrl Pts',(17.0702539988253,32.5663418025556,82.));
#5839=CARTESIAN_POINT('Ctrl Pts',(17.1416262957653,32.7296146052374,82.));
#5840=CARTESIAN_POINT('Ctrl Pts',(17.4226441511211,33.2098600173186,82.));
#5841=CARTESIAN_POINT('Ctrl Pts',(17.7820383793495,33.5422189915824,82.));
#5842=CARTESIAN_POINT('Ctrl Pts',(18.6622714155113,34.1331069213694,82.));
#5843=CARTESIAN_POINT('Ctrl Pts',(19.3931201505777,34.413210266344,82.));
#5844=CARTESIAN_POINT('Ctrl Pts',(20.6104592865239,34.7357198507857,82.));
#5845=CARTESIAN_POINT('Ctrl Pts',(21.2666393342951,34.845555358661,82.));
#5846=CARTESIAN_POINT('Ctrl Pts',(22.5901610524715,34.9770485861857,82.));
#5847=CARTESIAN_POINT('Ctrl Pts',(23.2573738737762,35.,82.));
#5848=CARTESIAN_POINT('Ctrl Pts',(23.8644712743399,35.,82.));
#5849=CARTESIAN_POINT('',(3.,35.,52.));
#5850=CARTESIAN_POINT('Origin',(35.,35.,52.));
#5851=CARTESIAN_POINT('Origin',(3.,32.,52.));
#5852=CARTESIAN_POINT('Origin',(35.,32.,52.));
#5853=CARTESIAN_POINT('Origin',(3.,32.,20.5));
#5854=CARTESIAN_POINT('',(3.,35.,11.));
#5855=CARTESIAN_POINT('Origin',(3.,32.,11.));
#5856=CARTESIAN_POINT('',(3.,35.,20.5));
#5857=CARTESIAN_POINT('Origin',(3.,38.,11.));
#5858=CARTESIAN_POINT('Origin',(3.,38.,11.));
#5859=CARTESIAN_POINT('Origin',(58.854497241083,38.,0.));
#5860=CARTESIAN_POINT('',(58.854497241083,35.,0.));
#5861=CARTESIAN_POINT('',(58.854497241083,35.,0.));
#5862=CARTESIAN_POINT('',(55.8685781532363,37.7096774193548,0.));
#5863=CARTESIAN_POINT('Origin',(58.854497241083,38.,0.));
#5864=CARTESIAN_POINT('',(55.8685781532363,37.7096774193548,0.));
#5865=CARTESIAN_POINT('Origin',(28.,49.,8.));
#5866=CARTESIAN_POINT('',(60.,38.,8.));
#5867=CARTESIAN_POINT('',(24.,50.,8.));
#5868=CARTESIAN_POINT('Origin',(28.,50.,8.));
#5869=CARTESIAN_POINT('Origin',(60.,38.,11.));
#5870=CARTESIAN_POINT('',(60.,35.,11.));
#5871=CARTESIAN_POINT('Origin',(92.,35.,41.));
#5872=CARTESIAN_POINT('',(31.47224362268,35.,82.));
#5873=CARTESIAN_POINT('',(158.47224362268,35.,52.7659032476128));
#5874=CARTESIAN_POINT('',(158.47224362268,35.,74.9975567301459));
#5875=CARTESIAN_POINT('',(180.509407751081,35.,52.9699515362416));
#5876=CARTESIAN_POINT('',(137.703021578879,35.,52.5735951906642));
#5877=CARTESIAN_POINT('',(180.898019313572,35.,11.));
#5878=CARTESIAN_POINT('',(180.542507983541,35.,49.3951347106504));
#5879=CARTESIAN_POINT('',(125.145502758917,35.,11.));
#5880=CARTESIAN_POINT('',(124.,35.,11.));
#5881=CARTESIAN_POINT('',(125.145502758917,35.,0.));
#5882=CARTESIAN_POINT('',(125.145502758917,35.,0.));
#5883=CARTESIAN_POINT('',(0.,35.,0.));
#5884=CARTESIAN_POINT('Origin',(35.,-32.,52.));
#5885=CARTESIAN_POINT('',(23.8644712743399,-35.,82.));
#5886=CARTESIAN_POINT('',(16.97224362268,-32.,82.));
#5887=CARTESIAN_POINT('Ctrl Pts',(23.8644712743399,-35.,82.));
#5888=CARTESIAN_POINT('Ctrl Pts',(23.2573738737762,-35.,82.));
#5889=CARTESIAN_POINT('Ctrl Pts',(22.5901610524715,-34.9770485861857,82.));
#5890=CARTESIAN_POINT('Ctrl Pts',(21.2666393342951,-34.845555358661,82.));
#5891=CARTESIAN_POINT('Ctrl Pts',(20.6104592865239,-34.7357198507857,82.));
#5892=CARTESIAN_POINT('Ctrl Pts',(19.3931201505777,-34.413210266344,82.));
#5893=CARTESIAN_POINT('Ctrl Pts',(18.6622714155113,-34.1331069213694,82.));
#5894=CARTESIAN_POINT('Ctrl Pts',(17.7820383793495,-33.5422189915824,82.));
#5895=CARTESIAN_POINT('Ctrl Pts',(17.4226441511211,-33.2098600173186,82.));
#5896=CARTESIAN_POINT('Ctrl Pts',(17.1416262957653,-32.7296146052374,82.));
#5897=CARTESIAN_POINT('Ctrl Pts',(17.0702539988253,-32.5663418025556,82.));
#5898=CARTESIAN_POINT('Ctrl Pts',(16.9946832528106,-32.2938517592452,82.));
#5899=CARTESIAN_POINT('Ctrl Pts',(16.97224362268,-32.1342826532508,82.));
#5900=CARTESIAN_POINT('Ctrl Pts',(16.97224362268,-32.,82.));
#5901=CARTESIAN_POINT('Origin',(35.,-32.,52.));
#5902=CARTESIAN_POINT('',(3.,-35.,52.));
#5903=CARTESIAN_POINT('Origin',(3.,-32.,52.));
#5904=CARTESIAN_POINT('Origin',(35.,-35.,52.));
#5905=CARTESIAN_POINT('Origin',(3.,-32.,20.5));
#5906=CARTESIAN_POINT('',(3.,-35.,11.));
#5907=CARTESIAN_POINT('Origin',(3.,-32.,11.));
#5908=CARTESIAN_POINT('',(3.,-35.,20.5));
#5909=CARTESIAN_POINT('Ctrl Pts',(5.55111512312578E-16,-34.9999999999998,
5.80384757729347));
#5910=CARTESIAN_POINT('Ctrl Pts',(-6.79692625904774E-15,-36.0180282120301,
5.27906287884847));
#5911=CARTESIAN_POINT('Ctrl Pts',(0.0612689060384735,-37.1929766938936,
5.));
#5912=CARTESIAN_POINT('Ctrl Pts',(0.20233103298048,-38.36,5.));
#5913=CARTESIAN_POINT('Ctrl Pts',(-2.7666680096006E-15,-35.4487989505127,
6.58119016196527));
#5914=CARTESIAN_POINT('Ctrl Pts',(0.016774360715285,-36.3253230330411,6.12605195674292));
#5915=CARTESIAN_POINT('Ctrl Pts',(0.0803150766662462,-37.3468098443969,
5.88545088698412));
#5916=CARTESIAN_POINT('Ctrl Pts',(0.20233103298048,-38.36,5.89759790102566));
#5917=CARTESIAN_POINT('Ctrl Pts',(0.752715575395041,-36.226020980098,7.92737820596885));
#5918=CARTESIAN_POINT('Ctrl Pts',(0.778729521784382,-36.8315954742153,7.59307849185768));
#5919=CARTESIAN_POINT('Ctrl Pts',(0.841952567680975,-37.5561034113538,7.42046619517227));
#5920=CARTESIAN_POINT('Ctrl Pts',(0.94960740409302,-38.2696741309526,7.45204196019633));
#5921=CARTESIAN_POINT('Ctrl Pts',(2.32680157423076,-36.4999999999999,8.40192378864674));
#5922=CARTESIAN_POINT('Ctrl Pts',(2.33447943710505,-36.9723882847684,8.12903347048555));
#5923=CARTESIAN_POINT('Ctrl Pts',(2.39172830825428,-37.5311331444668,7.98586184929931));
#5924=CARTESIAN_POINT('Ctrl Pts',(2.512318886995,-38.0807838110923,8.));
#5925=CARTESIAN_POINT('Ctrl Pts',(3.,-36.4999999999999,8.40192378864674));
#5926=CARTESIAN_POINT('Ctrl Pts',(2.99999999999999,-36.9544768803712,8.13953143942391));
#5927=CARTESIAN_POINT('Ctrl Pts',(3.05470438039141,-37.4790074526303,8.));
#5928=CARTESIAN_POINT('Ctrl Pts',(3.18065270801828,-38.,8.));
#5929=CARTESIAN_POINT('',(0.20233103298048,-38.36,5.));
#5930=CARTESIAN_POINT('',(3.18065270801828,-38.,8.));
#5931=CARTESIAN_POINT('Origin',(3.18065270801829,-38.,5.));
#5932=CARTESIAN_POINT('',(3.,-36.4999999999999,8.40192378864674));
#5933=CARTESIAN_POINT('Ctrl Pts',(3.18065270801828,-38.,8.));
#5934=CARTESIAN_POINT('Ctrl Pts',(3.05470438039141,-37.4790074526303,8.));
#5935=CARTESIAN_POINT('Ctrl Pts',(2.99999999999999,-36.9544768803712,8.13953143942391));
#5936=CARTESIAN_POINT('Ctrl Pts',(3.,-36.4999999999999,8.40192378864674));
#5937=CARTESIAN_POINT('Origin',(3.,-34.9999999999998,5.80384757729347));
#5938=CARTESIAN_POINT('Ctrl Pts',(5.55111512312578E-16,-34.9999999999998,
5.80384757729347));
#5939=CARTESIAN_POINT('Ctrl Pts',(-6.79692625904774E-15,-36.0180282120301,
5.27906287884847));
#5940=CARTESIAN_POINT('Ctrl Pts',(0.0612689060384735,-37.1929766938936,
5.));
#5941=CARTESIAN_POINT('Ctrl Pts',(0.20233103298048,-38.36,5.));
#5942=CARTESIAN_POINT('Origin',(28.,-35.,5.));
#5943=CARTESIAN_POINT('',(55.7976689670195,-38.36,5.));
#5944=CARTESIAN_POINT('',(52.8193472919817,-38.,8.));
#5945=CARTESIAN_POINT('Origin',(52.8193472919817,-38.,5.));
#5946=CARTESIAN_POINT('Origin',(28.,-35.,8.));
#5947=CARTESIAN_POINT('Origin',(28.,-35.,5.));
#5948=CARTESIAN_POINT('Ctrl Pts',(55.7976689670195,-38.36,5.));
#5949=CARTESIAN_POINT('Ctrl Pts',(55.8238771966224,-38.1431762825264,5.));
#5950=CARTESIAN_POINT('Ctrl Pts',(55.8475407647763,-37.926043434088,5.00937844175291));
#5951=CARTESIAN_POINT('Ctrl Pts',(55.8685781532363,-37.7096774193548,5.02816182430651));
#5952=CARTESIAN_POINT('Ctrl Pts',(55.7976689670195,-38.36,5.89759790102566));
#5953=CARTESIAN_POINT('Ctrl Pts',(55.8203385684754,-38.1717572674891,5.89534108170859));
#5954=CARTESIAN_POINT('Ctrl Pts',(55.8413719151341,-37.9830850669531,5.90163360405697));
#5955=CARTESIAN_POINT('Ctrl Pts',(55.8602609046479,-37.7952189272299,5.91625914580451));
#5956=CARTESIAN_POINT('Ctrl Pts',(55.0499325631178,-38.2696185252047,7.45169302838196));
#5957=CARTESIAN_POINT('Ctrl Pts',(55.0699339818664,-38.1370427186258,7.44582650050821));
#5958=CARTESIAN_POINT('Ctrl Pts',(55.0885194723629,-38.0040411687434,7.44665978236167));
#5959=CARTESIAN_POINT('Ctrl Pts',(55.1056560895983,-37.8713923378241,7.45429472319515));
#5960=CARTESIAN_POINT('Ctrl Pts',(53.487681113005,-38.0807838110923,8.));
#5961=CARTESIAN_POINT('Ctrl Pts',(53.51008589056,-37.9786630563262,7.99737324321024));
#5962=CARTESIAN_POINT('Ctrl Pts',(53.5304285848741,-37.8759649512515,8.00001814579442));
#5963=CARTESIAN_POINT('Ctrl Pts',(53.548732056513,-37.7738335502611,8.00784297571193));
#5964=CARTESIAN_POINT('Ctrl Pts',(52.8193472919817,-38.,8.));
#5965=CARTESIAN_POINT('Ctrl Pts',(52.8427474969842,-37.9032036975566,8.));
#5966=CARTESIAN_POINT('Ctrl Pts',(52.863875682836,-37.8062693902177,8.00468922087647));
#5967=CARTESIAN_POINT('Ctrl Pts',(52.8826590653895,-37.7096774193548,8.01408091215325));
#5968=CARTESIAN_POINT('',(55.8685781532363,-37.7096774193548,5.02816182430651));
#5969=CARTESIAN_POINT('',(52.8826590653895,-37.7096774193548,8.01408091215326));
#5970=CARTESIAN_POINT('Origin',(52.8826590653895,-37.4193548387097,5.02816182430651));
#5971=CARTESIAN_POINT('Ctrl Pts',(52.8826590653895,-37.7096774193548,8.01408091215325));
#5972=CARTESIAN_POINT('Ctrl Pts',(52.863875682836,-37.8062693902177,8.00468922087647));
#5973=CARTESIAN_POINT('Ctrl Pts',(52.8427474969842,-37.9032036975566,8.));
#5974=CARTESIAN_POINT('Ctrl Pts',(52.8193472919817,-38.,8.));
#5975=CARTESIAN_POINT('Ctrl Pts',(55.7976689670195,-38.36,5.));
#5976=CARTESIAN_POINT('Ctrl Pts',(55.8238771966224,-38.1431762825264,5.));
#5977=CARTESIAN_POINT('Ctrl Pts',(55.8475407647763,-37.926043434088,5.00937844175291));
#5978=CARTESIAN_POINT('Ctrl Pts',(55.8685781532363,-37.7096774193548,5.02816182430651));
#5979=CARTESIAN_POINT('Ctrl Pts',(58.854497241083,-35.,11.));
#5980=CARTESIAN_POINT('Ctrl Pts',(57.591179720436,-35.,10.3683412396765));
#5981=CARTESIAN_POINT('Ctrl Pts',(55.491665523271,-35.3447900318788,9.31858414109399));
#5982=CARTESIAN_POINT('Ctrl Pts',(53.4860813463977,-36.4709655486432,8.31579205265733));
#5983=CARTESIAN_POINT('Ctrl Pts',(52.9641634215603,-37.2905480972536,8.05483309023865));
#5984=CARTESIAN_POINT('Ctrl Pts',(52.8826590653895,-37.7096774193548,8.01408091215326));
#5985=CARTESIAN_POINT('Ctrl Pts',(58.854497241083,-35.,11.));
#5986=CARTESIAN_POINT('Ctrl Pts',(57.7114956747833,-35.,10.2480252853291));
#5987=CARTESIAN_POINT('Ctrl Pts',(55.8108578482975,-35.49734135073,9.00048604592416));
#5988=CARTESIAN_POINT('Ctrl Pts',(54.1695839772935,-36.8310361085116,8.12526335720806));
#5989=CARTESIAN_POINT('Ctrl Pts',(53.8246365954992,-37.4973792684685,8.02197912822726));
#5990=CARTESIAN_POINT('Ctrl Pts',(53.7707563868875,-37.7952189272299,8.00576366356483));
#5991=CARTESIAN_POINT('Ctrl Pts',(58.854497241083,-35.,11.));
#5992=CARTESIAN_POINT('Ctrl Pts',(57.9220485948912,-35.,10.0374723652213));
#5993=CARTESIAN_POINT('Ctrl Pts',(56.3761160372177,-35.6097541353715,8.44025943776391));
#5994=CARTESIAN_POINT('Ctrl Pts',(55.3639766415692,-37.1311590010604,7.3440863877359));
#5995=CARTESIAN_POINT('Ctrl Pts',(55.3169789816803,-37.677782831814,7.26436621839063));
#5996=CARTESIAN_POINT('Ctrl Pts',(55.3087758987271,-37.8713886997517,7.25113749710106));
#5997=CARTESIAN_POINT('Ctrl Pts',(58.854497241083,-35.,11.));
#5998=CARTESIAN_POINT('Ctrl Pts',(58.132601514999,-35.,9.82691944511346));
#5999=CARTESIAN_POINT('Ctrl Pts',(56.9368441486366,-35.4601371544742,7.87913897720146));
#6000=CARTESIAN_POINT('Ctrl Pts',(56.0284907858974,-36.7392653296661,6.14540023341453));
#6001=CARTESIAN_POINT('Ctrl Pts',(55.8851069427414,-37.4444604564192,5.75547550425093));
#6002=CARTESIAN_POINT('Ctrl Pts',(55.862340216795,-37.7738335502611,5.69423481543001));
#6003=CARTESIAN_POINT('Ctrl Pts',(58.854497241083,-35.,11.));
#6004=CARTESIAN_POINT('Ctrl Pts',(58.2228384807595,-35.,9.73668247935295));
#6005=CARTESIAN_POINT('Ctrl Pts',(57.173081382177,-35.3447900318788,7.63716828218798));
#6006=CARTESIAN_POINT('Ctrl Pts',(56.1702892937404,-36.4709655486432,5.63158410531467));
#6007=CARTESIAN_POINT('Ctrl Pts',(55.9093303313217,-37.2905480972536,5.10966618047728));
#6008=CARTESIAN_POINT('Ctrl Pts',(55.8685781532363,-37.7096774193548,5.02816182430651));
#6009=CARTESIAN_POINT('',(58.854497241083,-35.,11.));
#6010=CARTESIAN_POINT('Origin',(58.854497241083,-38.,11.));
#6011=CARTESIAN_POINT('Origin',(58.854497241083,-38.,11.));
#6012=CARTESIAN_POINT('Origin',(3.,-38.,11.));
#6013=CARTESIAN_POINT('Origin',(3.,-38.,11.));
#6014=CARTESIAN_POINT('Origin',(28.,-49.,8.));
#6015=CARTESIAN_POINT('',(60.,-38.,8.));
#6016=CARTESIAN_POINT('',(24.,-50.,8.));
#6017=CARTESIAN_POINT('Origin',(28.,-50.,8.));
#6018=CARTESIAN_POINT('Origin',(58.854497241083,-38.,0.));
#6019=CARTESIAN_POINT('',(55.8685781532363,-37.7096774193548,0.));
#6020=CARTESIAN_POINT('',(58.854497241083,-35.,0.));
#6021=CARTESIAN_POINT('Origin',(28.,-35.,0.));
#6022=CARTESIAN_POINT('Ctrl Pts',(125.145502758917,35.,11.));
#6023=CARTESIAN_POINT('Ctrl Pts',(126.408820279564,35.,10.3683412396765));
#6024=CARTESIAN_POINT('Ctrl Pts',(128.508262002194,35.3448821043614,9.31862037836163));
#6025=CARTESIAN_POINT('Ctrl Pts',(130.513866046969,36.4710105181724,8.31581835597387));
#6026=CARTESIAN_POINT('Ctrl Pts',(131.03583657844,37.2905480972536,8.05483309023865));
#6027=CARTESIAN_POINT('Ctrl Pts',(131.11734093461,37.7096774193548,8.01408091215326));
#6028=CARTESIAN_POINT('Ctrl Pts',(125.145502758917,35.,11.));
#6029=CARTESIAN_POINT('Ctrl Pts',(126.288504325217,35.,10.2480252853291));
#6030=CARTESIAN_POINT('Ctrl Pts',(128.189273783442,35.4974603268054,9.00013278294707));
#6031=CARTESIAN_POINT('Ctrl Pts',(129.830512389917,36.8310532862727,8.12500325624924));
#6032=CARTESIAN_POINT('Ctrl Pts',(130.175363404501,37.4973792684685,8.02197912822726));
#6033=CARTESIAN_POINT('Ctrl Pts',(130.229243613112,37.7952189272299,8.00576366356483));
#6034=CARTESIAN_POINT('Ctrl Pts',(125.145502758917,35.,11.));
#6035=CARTESIAN_POINT('Ctrl Pts',(126.077951405109,35.,10.0374723652213));
#6036=CARTESIAN_POINT('Ctrl Pts',(127.623980299275,35.6097041403199,8.44014872177682));
#6037=CARTESIAN_POINT('Ctrl Pts',(128.636157969133,37.1308061894763,7.34393528770233));
#6038=CARTESIAN_POINT('Ctrl Pts',(128.683173815107,37.6777482307114,7.26416314863648));
#6039=CARTESIAN_POINT('Ctrl Pts',(128.69137689806,37.8713540986491,7.25093442734691));
#6040=CARTESIAN_POINT('Ctrl Pts',(125.145502758917,35.,11.));
#6041=CARTESIAN_POINT('Ctrl Pts',(125.867398485001,35.,9.82691944511346));
#6042=CARTESIAN_POINT('Ctrl Pts',(127.063224468555,35.4602324624254,7.87926400736172));
#6043=CARTESIAN_POINT('Ctrl Pts',(127.971574547182,36.7392080834518,6.14547579678636));
#6044=CARTESIAN_POINT('Ctrl Pts',(128.114893057259,37.4444604564192,5.75547550425093));
#6045=CARTESIAN_POINT('Ctrl Pts',(128.137659783205,37.7738335502611,5.69423481543001));
#6046=CARTESIAN_POINT('Ctrl Pts',(125.145502758917,35.,11.));
#6047=CARTESIAN_POINT('Ctrl Pts',(125.777161519241,35.,9.73668247935295));
#6048=CARTESIAN_POINT('Ctrl Pts',(126.826882380555,35.3448821043614,7.63724075672326));
#6049=CARTESIAN_POINT('Ctrl Pts',(127.829684402943,36.4710105181724,5.63163671194773));
#6050=CARTESIAN_POINT('Ctrl Pts',(128.090669668678,37.2905480972536,5.10966618047728));
#6051=CARTESIAN_POINT('Ctrl Pts',(128.131421846764,37.7096774193548,5.02816182430651));
#6052=CARTESIAN_POINT('',(131.11734093461,37.7096774193548,8.01408091215326));
#6053=CARTESIAN_POINT('',(128.131421846764,37.7096774193548,5.02816182430653));
#6054=CARTESIAN_POINT('Origin',(131.11734093461,37.4193548387097,5.02816182430651));
#6055=CARTESIAN_POINT('Origin',(125.145502758917,38.,11.));
#6056=CARTESIAN_POINT('Origin',(125.145502758917,38.,11.));
#6057=CARTESIAN_POINT('Ctrl Pts',(128.20233103298,38.36,5.));
#6058=CARTESIAN_POINT('Ctrl Pts',(128.176122803378,38.1431762825264,5.));
#6059=CARTESIAN_POINT('Ctrl Pts',(128.152459235224,37.926043434088,5.00937844175291));
#6060=CARTESIAN_POINT('Ctrl Pts',(128.131421846764,37.7096774193548,5.02816182430651));
#6061=CARTESIAN_POINT('Ctrl Pts',(128.20233103298,38.36,5.89759790102566));
#6062=CARTESIAN_POINT('Ctrl Pts',(128.179661431525,38.1717572674891,5.89534108170859));
#6063=CARTESIAN_POINT('Ctrl Pts',(128.158628084866,37.9830850669535,5.90163360405693));
#6064=CARTESIAN_POINT('Ctrl Pts',(128.139739095352,37.7952189272299,5.91625914580451));
#6065=CARTESIAN_POINT('Ctrl Pts',(128.950298064189,38.2695906484878,7.45151809910225));
#6066=CARTESIAN_POINT('Ctrl Pts',(128.93029664544,38.137014841909,7.4456515712285));
#6067=CARTESIAN_POINT('Ctrl Pts',(128.91170554589,38.0040028278322,7.44649047075606));
#6068=CARTESIAN_POINT('Ctrl Pts',(128.894568928654,37.8713539969117,7.45412541158964));
#6069=CARTESIAN_POINT('Ctrl Pts',(130.512318886995,38.0807838110923,8.00000000000001));
#6070=CARTESIAN_POINT('Ctrl Pts',(130.48991410944,37.9786630563264,7.99737324321024));
#6071=CARTESIAN_POINT('Ctrl Pts',(130.469571415126,37.8759649512528,8.00001814579429));
#6072=CARTESIAN_POINT('Ctrl Pts',(130.451267943487,37.7738335502611,8.00784297571193));
#6073=CARTESIAN_POINT('Ctrl Pts',(131.180652708018,38.,8.00000000000001));
#6074=CARTESIAN_POINT('Ctrl Pts',(131.157252503016,37.9032036975568,8.00000000000001));
#6075=CARTESIAN_POINT('Ctrl Pts',(131.136124317164,37.806269390219,8.00468922087635));
#6076=CARTESIAN_POINT('Ctrl Pts',(131.11734093461,37.7096774193548,8.01408091215326));
#6077=CARTESIAN_POINT('',(131.180652708018,38.,8.));
#6078=CARTESIAN_POINT('Ctrl Pts',(131.11734093461,37.7096774193548,8.01408091215326));
#6079=CARTESIAN_POINT('Ctrl Pts',(131.136124317164,37.806269390219,8.00468922087635));
#6080=CARTESIAN_POINT('Ctrl Pts',(131.157252503016,37.9032036975568,8.00000000000001));
#6081=CARTESIAN_POINT('Ctrl Pts',(131.180652708018,38.,8.00000000000001));
#6082=CARTESIAN_POINT('',(128.20233103298,38.36,5.));
#6083=CARTESIAN_POINT('Origin',(131.180652708018,38.,5.));
#6084=CARTESIAN_POINT('Ctrl Pts',(128.20233103298,38.36,5.));
#6085=CARTESIAN_POINT('Ctrl Pts',(128.176122803378,38.1431762825264,5.));
#6086=CARTESIAN_POINT('Ctrl Pts',(128.152459235224,37.926043434088,5.00937844175291));
#6087=CARTESIAN_POINT('Ctrl Pts',(128.131421846764,37.7096774193548,5.02816182430651));
#6088=CARTESIAN_POINT('Origin',(156.,35.,5.));
#6089=CARTESIAN_POINT('',(180.819347291982,38.,8.));
#6090=CARTESIAN_POINT('',(183.79766896702,38.36,5.));
#6091=CARTESIAN_POINT('Origin',(180.819347291982,38.,5.));
#6092=CARTESIAN_POINT('Origin',(156.,35.,5.));
#6093=CARTESIAN_POINT('Origin',(156.,35.,8.));
#6094=CARTESIAN_POINT('Ctrl Pts',(183.969815620835,33.7002253516408,6.67679159415515));
#6095=CARTESIAN_POINT('Ctrl Pts',(183.994326048599,34.2276645859955,6.2235861382656));
#6096=CARTESIAN_POINT('Ctrl Pts',(184.02615428097,35.6677168210592,5.33752658855133));
#6097=CARTESIAN_POINT('Ctrl Pts',(183.914814816133,37.390838829013,5.));
#6098=CARTESIAN_POINT('Ctrl Pts',(183.79766896702,38.36,5.));
#6099=CARTESIAN_POINT('Ctrl Pts',(183.999283936978,34.3343532523772,7.33713979338968));
#6100=CARTESIAN_POINT('Ctrl Pts',(184.007758579302,34.7839174007239,6.94606885961919));
#6101=CARTESIAN_POINT('Ctrl Pts',(184.00754893802,36.0206255096479,6.17500497055533));
#6102=CARTESIAN_POINT('Ctrl Pts',(183.898997814937,37.5185904475954,5.88751034382702));
#6103=CARTESIAN_POINT('Ctrl Pts',(183.79766896702,38.36,5.89759790102566));
#6104=CARTESIAN_POINT('Ctrl Pts',(183.264452217124,35.4676246877956,8.47924395641892));
#6105=CARTESIAN_POINT('Ctrl Pts',(183.263208393294,35.7681924393132,8.19574897233831));
#6106=CARTESIAN_POINT('Ctrl Pts',(183.243967632483,36.6145825085804,7.62528081991518));
#6107=CARTESIAN_POINT('Ctrl Pts',(183.139031868617,37.6769929878661,7.42524072691035));
#6108=CARTESIAN_POINT('Ctrl Pts',(183.049629294758,38.2695818681135,7.451463001346));
#6109=CARTESIAN_POINT('Ctrl Pts',(181.659660906753,35.90317816407,8.8543376916631));
#6110=CARTESIAN_POINT('Ctrl Pts',(181.674727762002,36.1417795639035,8.62106214617757));
#6111=CARTESIAN_POINT('Ctrl Pts',(181.689017399754,36.8060222478378,8.15740575482789));
#6112=CARTESIAN_POINT('Ctrl Pts',(181.587826247974,37.6243232752034,7.98825889198873));
#6113=CARTESIAN_POINT('Ctrl Pts',(181.487681113005,38.0807838110923,8.00000000000001));
#6114=CARTESIAN_POINT('Ctrl Pts',(180.973049661459,35.9197434605539,8.83839579707757));
#6115=CARTESIAN_POINT('Ctrl Pts',(180.994933971964,36.1552074044623,8.6117930691328));
#6116=CARTESIAN_POINT('Ctrl Pts',(181.023352036581,36.7980878665444,8.16876329427566));
#6117=CARTESIAN_POINT('Ctrl Pts',(180.923941800119,37.567338762952,8.00000000000001));
#6118=CARTESIAN_POINT('Ctrl Pts',(180.819347291982,38.,8.00000000000001));
#6119=CARTESIAN_POINT('',(183.402520572671,35.,8.));
#6120=CARTESIAN_POINT('',(184.,35.0000000000057,5.80384757728751));
#6121=CARTESIAN_POINT('Ctrl Pts',(183.402520572671,35.,8.00000000000001));
#6122=CARTESIAN_POINT('Ctrl Pts',(183.547773995999,35.,7.7333080978234));
#6123=CARTESIAN_POINT('Ctrl Pts',(183.671610877184,35.,7.45631037055478));
#6124=CARTESIAN_POINT('Ctrl Pts',(183.917381012336,35.,6.72638475914925));
#6125=CARTESIAN_POINT('Ctrl Pts',(184.,35.,6.2679088960418));
#6126=CARTESIAN_POINT('Ctrl Pts',(184.,35.,5.80384757729336));
#6127=CARTESIAN_POINT('Ctrl Pts',(184.000120745918,35.000102047304,5.80404540408506));
#6128=CARTESIAN_POINT('Ctrl Pts',(184.000133528268,35.1673874095417,5.71774484775865));
#6129=CARTESIAN_POINT('Ctrl Pts',(183.99092210883,36.2129801855919,5.23071994198585));
#6130=CARTESIAN_POINT('Ctrl Pts',(183.914814816133,37.390838829013,5.));
#6131=CARTESIAN_POINT('Ctrl Pts',(183.79766896702,38.36,5.));
#6132=CARTESIAN_POINT('',(180.951927409851,37.2748094254573,8.0889694899422));
#6133=CARTESIAN_POINT('Ctrl Pts',(180.819347291982,38.,8.00000000000001));
#6134=CARTESIAN_POINT('Ctrl Pts',(180.877934687157,37.7576498487013,8.00000000000001));
#6135=CARTESIAN_POINT('Ctrl Pts',(180.921528153108,37.5131314297474,8.03025732712463));
#6136=CARTESIAN_POINT('Ctrl Pts',(180.951190744332,37.2749112313906,8.08956288864171));
#6137=CARTESIAN_POINT('',(181.667890676754,37.2737119676904,8.));
#6138=CARTESIAN_POINT('Ctrl Pts',(180.951927410773,37.2748094100323,8.08896949376647));
#6139=CARTESIAN_POINT('Ctrl Pts',(180.956018127086,37.274924346416,8.088940861025));
#6140=CARTESIAN_POINT('Ctrl Pts',(180.960108840395,37.2750372329885,8.08890412577989));
#6141=CARTESIAN_POINT('Ctrl Pts',(181.201858997869,37.2815874148225,8.08625432298268));
#6142=CARTESIAN_POINT('Ctrl Pts',(181.438060925305,37.2810667321981,8.05631843825027));
#6143=CARTESIAN_POINT('Ctrl Pts',(181.667890676754,37.2737119676901,8.00000000000007));
#6144=CARTESIAN_POINT('Ctrl Pts',(181.667890676754,37.2737119676904,8.));
#6145=CARTESIAN_POINT('Ctrl Pts',(181.971820880737,36.9900034700373,8.));
#6146=CARTESIAN_POINT('Ctrl Pts',(182.272427380856,36.6776626323208,7.99999999958518));
#6147=CARTESIAN_POINT('Ctrl Pts',(182.944484312768,35.8457345941287,7.99999999958518));
#6148=CARTESIAN_POINT('Ctrl Pts',(183.212875666898,35.3970112792475,8.));
#6149=CARTESIAN_POINT('Ctrl Pts',(183.402520572671,35.,8.));
#6150=CARTESIAN_POINT('Origin',(156.,35.,0.));
#6151=CARTESIAN_POINT('',(184.,35.,0.));
#6152=CARTESIAN_POINT('',(184.,35.,0.));
#6153=CARTESIAN_POINT('',(128.131421846764,37.7096774193548,0.));
#6154=CARTESIAN_POINT('Origin',(156.,35.,0.));
#6155=CARTESIAN_POINT('',(128.131421846764,37.7096774193548,0.));
#6156=CARTESIAN_POINT('Origin',(128.,35.,0.));
#6157=CARTESIAN_POINT('',(183.368772894521,35.,7.99999999999765));
#6158=CARTESIAN_POINT('',(142.,35.,8.));
#6159=CARTESIAN_POINT('',(183.946003354294,35.,5.83162422873126));
#6160=CARTESIAN_POINT('Ctrl Pts',(183.36877289452,35.,7.99999999999716));
#6161=CARTESIAN_POINT('Ctrl Pts',(183.466406037598,35.,7.81137594025211));
#6162=CARTESIAN_POINT('Ctrl Pts',(183.555890991522,35.,7.61467203113216));
#6163=CARTESIAN_POINT('Ctrl Pts',(183.851877965836,35.,6.8386327440255));
#6164=CARTESIAN_POINT('Ctrl Pts',(183.941587367144,35.,6.30854973630244));
#6165=CARTESIAN_POINT('Ctrl Pts',(183.946003354294,35.,5.83162422873126));
#6166=CARTESIAN_POINT('',(184.,35.,0.));
#6167=CARTESIAN_POINT('Origin',(156.,49.,8.));
#6168=CARTESIAN_POINT('Ctrl Pts',(181.667890676754,37.2737119676904,8.));
#6169=CARTESIAN_POINT('Ctrl Pts',(181.974263430434,36.9523898924629,8.));
#6170=CARTESIAN_POINT('Ctrl Pts',(182.271552717037,36.6215018559916,8.));
#6171=CARTESIAN_POINT('Ctrl Pts',(182.837203794954,35.9007967977578,8.));
#6172=CARTESIAN_POINT('Ctrl Pts',(183.128758753871,35.475688585275,8.));
#6173=CARTESIAN_POINT('Ctrl Pts',(183.368772894519,34.999999999999,8.));
#6174=CARTESIAN_POINT('Ctrl Pts',(183.897890720421,32.,11.0277766514379));
#6175=CARTESIAN_POINT('Ctrl Pts',(183.908476258216,32.,9.88454121758138));
#6176=CARTESIAN_POINT('Ctrl Pts',(183.933198048223,32.7822331288304,7.21459408111487));
#6177=CARTESIAN_POINT('Ctrl Pts',(183.948579057724,35.1094518511976,5.5534489026464));
#6178=CARTESIAN_POINT('Ctrl Pts',(183.951893158078,36.5911484250779,5.19552689342517));
#6179=CARTESIAN_POINT('Ctrl Pts',(183.897890720421,32.8975979010257,11.0277766514379));
#6180=CARTESIAN_POINT('Ctrl Pts',(183.906848467244,32.8965695980516,10.0562409853862));
#6181=CARTESIAN_POINT('Ctrl Pts',(183.92786931383,33.5598355037628,7.78441731032418));
#6182=CARTESIAN_POINT('Ctrl Pts',(183.94105067019,35.5403566750075,6.36777674722119));
#6183=CARTESIAN_POINT('Ctrl Pts',(183.94386106412,36.80071300929,6.06299103161509));
#6184=CARTESIAN_POINT('Ctrl Pts',(183.144438752334,34.4514631268444,11.0208002281669));
#6185=CARTESIAN_POINT('Ctrl Pts',(183.152499885901,34.448790086954,10.3444760457849));
#6186=CARTESIAN_POINT('Ctrl Pts',(183.171343341433,34.905148868596,8.76122121233146));
#6187=CARTESIAN_POINT('Ctrl Pts',(183.183090568948,36.2839134347555,7.77152178690107));
#6188=CARTESIAN_POINT('Ctrl Pts',(183.185625354358,37.1635876050048,7.55816920506391));
#6189=CARTESIAN_POINT('Ctrl Pts',(181.571188883105,35.,11.006233066007));
#6190=CARTESIAN_POINT('Ctrl Pts',(181.581029357879,34.9988031377618,10.4350067310519));
#6191=CARTESIAN_POINT('Ctrl Pts',(181.603998038734,35.3874005905622,9.09836594332551));
#6192=CARTESIAN_POINT('Ctrl Pts',(181.618277315131,36.5524153149342,8.26377751595704));
#6193=CARTESIAN_POINT('Ctrl Pts',(181.621361391319,37.2941596483767,8.08421682634416));
#6194=CARTESIAN_POINT('Ctrl Pts',(180.898019313572,35.,11.));
#6195=CARTESIAN_POINT('Ctrl Pts',(180.908604851367,35.,10.4283822830717));
#6196=CARTESIAN_POINT('Ctrl Pts',(180.933326641373,35.3911165644152,9.09340871483851));
#6197=CARTESIAN_POINT('Ctrl Pts',(180.948707650874,36.5547259255988,8.26283612560427));
#6198=CARTESIAN_POINT('Ctrl Pts',(180.952021751228,37.2955742125389,8.08387512099366));
#6199=CARTESIAN_POINT('Origin',(180.898019313572,38.,11.));
#6200=CARTESIAN_POINT('',(183.897890720421,32.,11.0277766514379));
#6201=CARTESIAN_POINT('Origin',(180.898019313572,32.,11.));
#6202=CARTESIAN_POINT('Origin',(183.897890720421,38.,11.0277766514379));
#6203=CARTESIAN_POINT('Origin',(156.,-35.,5.));
#6204=CARTESIAN_POINT('',(131.180652708018,-38.,8.));
#6205=CARTESIAN_POINT('',(128.20233103298,-38.36,5.));
#6206=CARTESIAN_POINT('Origin',(131.180652708018,-38.,5.));
#6207=CARTESIAN_POINT('',(183.79766896702,-38.36,5.));
#6208=CARTESIAN_POINT('Origin',(156.,-35.,5.));
#6209=CARTESIAN_POINT('',(180.819347291982,-38.,8.));
#6210=CARTESIAN_POINT('Origin',(180.819347291982,-38.,5.));
#6211=CARTESIAN_POINT('Origin',(156.,-35.,8.));
#6212=CARTESIAN_POINT('Ctrl Pts',(128.131421846764,-37.7096774193548,5.02816182430651));
#6213=CARTESIAN_POINT('Ctrl Pts',(128.152459235224,-37.926043434088,5.00937844175291));
#6214=CARTESIAN_POINT('Ctrl Pts',(128.176122803378,-38.1431762825264,5.));
#6215=CARTESIAN_POINT('Ctrl Pts',(128.20233103298,-38.36,5.));
#6216=CARTESIAN_POINT('Ctrl Pts',(128.139739095352,-37.7952189272299,5.91625914580451));
#6217=CARTESIAN_POINT('Ctrl Pts',(128.158628084866,-37.9830850669534,5.90163360405695));
#6218=CARTESIAN_POINT('Ctrl Pts',(128.179661431525,-38.1717572674893,5.89534108170859));
#6219=CARTESIAN_POINT('Ctrl Pts',(128.20233103298,-38.36,5.89759790102566));
#6220=CARTESIAN_POINT('Ctrl Pts',(128.894568928654,-37.8713539969118,7.45412541158965));
#6221=CARTESIAN_POINT('Ctrl Pts',(128.91170554589,-38.0040028278317,7.44649047075611));
#6222=CARTESIAN_POINT('Ctrl Pts',(128.93029664544,-38.1370148419096,7.4456515712285));
#6223=CARTESIAN_POINT('Ctrl Pts',(128.950298064189,-38.2695906484878,7.45151809910225));
#6224=CARTESIAN_POINT('Ctrl Pts',(130.451267943487,-37.7738335502611,8.00784297571193));
#6225=CARTESIAN_POINT('Ctrl Pts',(130.469571415126,-37.8759649512522,8.00001814579435));
#6226=CARTESIAN_POINT('Ctrl Pts',(130.48991410944,-37.978663056327,7.99737324321024));
#6227=CARTESIAN_POINT('Ctrl Pts',(130.512318886995,-38.0807838110923,8.00000000000001));
#6228=CARTESIAN_POINT('Ctrl Pts',(131.11734093461,-37.7096774193548,8.01408091215325));
#6229=CARTESIAN_POINT('Ctrl Pts',(131.136124317164,-37.8062693902184,8.0046892208764));
#6230=CARTESIAN_POINT('Ctrl Pts',(131.157252503016,-37.9032036975574,8.00000000000001));
#6231=CARTESIAN_POINT('Ctrl Pts',(131.180652708018,-38.,8.00000000000001));
#6232=CARTESIAN_POINT('',(131.11734093461,-37.7096774193548,8.01408091215326));
#6233=CARTESIAN_POINT('Ctrl Pts',(131.180652708018,-38.,8.00000000000001));
#6234=CARTESIAN_POINT('Ctrl Pts',(131.157252503016,-37.9032036975574,8.00000000000001));
#6235=CARTESIAN_POINT('Ctrl Pts',(131.136124317164,-37.8062693902184,8.0046892208764));
#6236=CARTESIAN_POINT('Ctrl Pts',(131.11734093461,-37.7096774193548,8.01408091215325));
#6237=CARTESIAN_POINT('',(128.131421846764,-37.7096774193548,5.02816182430651));
#6238=CARTESIAN_POINT('Origin',(131.11734093461,-37.4193548387097,5.02816182430651));
#6239=CARTESIAN_POINT('Ctrl Pts',(128.131421846764,-37.7096774193548,5.02816182430651));
#6240=CARTESIAN_POINT('Ctrl Pts',(128.152459235224,-37.926043434088,5.00937844175291));
#6241=CARTESIAN_POINT('Ctrl Pts',(128.176122803378,-38.1431762825264,5.));
#6242=CARTESIAN_POINT('Ctrl Pts',(128.20233103298,-38.36,5.));
#6243=CARTESIAN_POINT('Ctrl Pts',(131.11734093461,-37.7096774193548,8.01408091215326));
#6244=CARTESIAN_POINT('Ctrl Pts',(131.076588756525,-37.5001127583042,8.03445700119595));
#6245=CARTESIAN_POINT('Ctrl Pts',(130.822486477689,-36.8777394142145,8.16150814061386));
#6246=CARTESIAN_POINT('Ctrl Pts',(129.756916368741,-35.9426049163746,8.69429319508786));
#6247=CARTESIAN_POINT('Ctrl Pts',(127.671636697566,-35.1800834699449,9.73693303067528));
#6248=CARTESIAN_POINT('Ctrl Pts',(125.987714439348,-35.,10.5788941597843));
#6249=CARTESIAN_POINT('Ctrl Pts',(125.145502758917,-35.,11.));
#6250=CARTESIAN_POINT('Ctrl Pts',(130.229243613112,-37.7952189272299,8.00576366356483));
#6251=CARTESIAN_POINT('Ctrl Pts',(130.202303508807,-37.6462990978492,8.01387139589604));
#6252=CARTESIAN_POINT('Ctrl Pts',(130.035901503225,-37.1878650592641,8.06332025121927));
#6253=CARTESIAN_POINT('Ctrl Pts',(129.236458211218,-36.2429002783718,8.41304981555658));
#6254=CARTESIAN_POINT('Ctrl Pts',(127.431915327519,-35.2514546514263,9.49424407278561));
#6255=CARTESIAN_POINT('Ctrl Pts',(125.907503803117,-35.,10.4986835235528));
#6256=CARTESIAN_POINT('Ctrl Pts',(125.145502758917,-35.,11.));
#6257=CARTESIAN_POINT('Ctrl Pts',(128.69137689806,-37.8713540986491,7.25093442734691));
#6258=CARTESIAN_POINT('Ctrl Pts',(128.687275356584,-37.7745511646802,7.25754878799169));
#6259=CARTESIAN_POINT('Ctrl Pts',(128.667694768037,-37.4546169089802,7.29289324516655));
#6260=CARTESIAN_POINT('Ctrl Pts',(128.321536446058,-36.4828470073741,7.69451037570431));
#6261=CARTESIAN_POINT('Ctrl Pts',(127.009479360979,-35.3039679777576,9.07589627680508));
#6262=CARTESIAN_POINT('Ctrl Pts',(125.767135189712,-35.,10.3583149101475));
#6263=CARTESIAN_POINT('Ctrl Pts',(125.145502758917,-35.,11.));
#6264=CARTESIAN_POINT('Ctrl Pts',(128.137659783205,-37.7738335502611,5.69423481543001));
#6265=CARTESIAN_POINT('Ctrl Pts',(128.126276420232,-37.6091470033402,5.72485515984047));
#6266=CARTESIAN_POINT('Ctrl Pts',(128.056978238003,-37.1082707099995,5.91366148966411));
#6267=CARTESIAN_POINT('Ctrl Pts',(127.660173748571,-36.1672395340187,6.78108593159827));
#6268=CARTESIAN_POINT('Ctrl Pts',(126.589351201994,-35.2341452946653,8.65501989450532));
#6269=CARTESIAN_POINT('Ctrl Pts',(125.626766576306,-35.,10.2179462967423));
#6270=CARTESIAN_POINT('Ctrl Pts',(125.145502758917,-35.,11.));
#6271=CARTESIAN_POINT('Ctrl Pts',(128.131421846764,-37.7096774193548,5.02816182430651));
#6272=CARTESIAN_POINT('Ctrl Pts',(128.111045757721,-37.5001127583042,5.0689140023919));
#6273=CARTESIAN_POINT('Ctrl Pts',(127.983994618303,-36.8777394142145,5.32301628122771));
#6274=CARTESIAN_POINT('Ctrl Pts',(127.451209563829,-35.9426049163746,6.38858639017571));
#6275=CARTESIAN_POINT('Ctrl Pts',(126.408569728242,-35.1800834699449,8.47386606135057));
#6276=CARTESIAN_POINT('Ctrl Pts',(125.566608599133,-35.,10.1577883195686));
#6277=CARTESIAN_POINT('Ctrl Pts',(125.145502758917,-35.,11.));
#6278=CARTESIAN_POINT('',(125.145502758917,-35.,11.));
#6279=CARTESIAN_POINT('Origin',(125.145502758917,-38.,11.));
#6280=CARTESIAN_POINT('Origin',(125.145502758917,-38.,11.));
#6281=CARTESIAN_POINT('Ctrl Pts',(180.973049661459,-35.9197434605539,8.83839579707758));
#6282=CARTESIAN_POINT('Ctrl Pts',(181.024369346261,-36.4719169174759,8.30700228705497));
#6283=CARTESIAN_POINT('Ctrl Pts',(181.00314731485,-37.2397005666917,8.));
#6284=CARTESIAN_POINT('Ctrl Pts',(180.819347291982,-38.,8.));
#6285=CARTESIAN_POINT('Ctrl Pts',(181.888531321851,-35.8976563985753,8.85965165652495));
#6286=CARTESIAN_POINT('Ctrl Pts',(181.917708840364,-36.4582452641848,8.30800657542114));
#6287=CARTESIAN_POINT('Ctrl Pts',(181.883286339303,-37.2926975054263,7.971937985194));
#6288=CARTESIAN_POINT('Ctrl Pts',(181.710459053346,-38.1077117481231,8.));
#6289=CARTESIAN_POINT('Ctrl Pts',(183.471901157116,-35.3139801735237,8.32960849046661));
#6290=CARTESIAN_POINT('Ctrl Pts',(183.466030118439,-36.0687832506354,7.63040959063072));
#6291=CARTESIAN_POINT('Ctrl Pts',(183.409166117026,-37.1880560548143,7.20299655425038));
#6292=CARTESIAN_POINT('Ctrl Pts',(183.253095761512,-38.2941755608114,7.24651557480386));
#6293=CARTESIAN_POINT('Ctrl Pts',(183.991916857942,-34.1758212771931,7.17205274358105));
#6294=CARTESIAN_POINT('Ctrl Pts',(184.021762067457,-35.2769187438743,6.2180368164864));
#6295=CARTESIAN_POINT('Ctrl Pts',(183.983057240361,-36.8243680976585,5.66035404348166));
#6296=CARTESIAN_POINT('Ctrl Pts',(183.79766896702,-38.36,5.67319842576924));
#6297=CARTESIAN_POINT('Ctrl Pts',(183.969815620835,-33.7002253516408,6.67679159415515));
#6298=CARTESIAN_POINT('Ctrl Pts',(184.027293667812,-34.9370938951461,5.61400457410994));
#6299=CARTESIAN_POINT('Ctrl Pts',(184.003524992632,-36.6569292693893,5.));
#6300=CARTESIAN_POINT('Ctrl Pts',(183.79766896702,-38.36,5.));
#6301=CARTESIAN_POINT('',(181.667890676754,-37.2737119676905,8.));
#6302=CARTESIAN_POINT('',(180.951927410069,-37.2748094218035,8.08896949084808));
#6303=CARTESIAN_POINT('Ctrl Pts',(181.666636694743,-37.2729596773495,7.99687411834348));
#6304=CARTESIAN_POINT('Ctrl Pts',(181.569302349961,-37.2762121398385,8.02134483314431));
#6305=CARTESIAN_POINT('Ctrl Pts',(181.470885453719,-37.2782472631398,8.04110399082257));
#6306=CARTESIAN_POINT('Ctrl Pts',(181.371712379837,-37.2790308976767,8.05596775956708));
#6307=CARTESIAN_POINT('Ctrl Pts',(181.27436640165,-37.2798000950764,8.07055768858045));
#6308=CARTESIAN_POINT('Ctrl Pts',(181.176291132015,-37.2793632927185,8.08043120267881));
#6309=CARTESIAN_POINT('Ctrl Pts',(181.077788864619,-37.2776661013203,8.08537023158407));
#6310=CARTESIAN_POINT('Ctrl Pts',(181.0399937172,-37.2770148919544,8.08726532832156));
#6311=CARTESIAN_POINT('Ctrl Pts',(181.002135693703,-37.2761779038092,8.08843345948832));
#6312=CARTESIAN_POINT('Ctrl Pts',(180.964231951489,-37.2751512711449,8.08886040524177));
#6313=CARTESIAN_POINT('Ctrl Pts',(180.960130633245,-37.2750401858792,8.08890660227419));
#6314=CARTESIAN_POINT('Ctrl Pts',(180.956029091187,-37.2749268986846,8.08894411433519));
#6315=CARTESIAN_POINT('Ctrl Pts',(180.951927347206,-37.2748114061892,8.08897292638101));
#6316=CARTESIAN_POINT('Ctrl Pts',(180.948784580753,-37.2752662540447,8.09156800850377));
#6317=CARTESIAN_POINT('Ctrl Pts',(180.920314453382,-37.512739598246,8.03142446135659));
#6318=CARTESIAN_POINT('Ctrl Pts',(180.87815153677,-37.7567528377248,8.));
#6319=CARTESIAN_POINT('Ctrl Pts',(180.819347291982,-38.,8.));
#6320=CARTESIAN_POINT('',(184.,-35.0000000018351,5.8038475754014));
#6321=CARTESIAN_POINT('Ctrl Pts',(183.79766896702,-38.36,5.));
#6322=CARTESIAN_POINT('Ctrl Pts',(183.938441824961,-37.1953698498218,5.));
#6323=CARTESIAN_POINT('Ctrl Pts',(183.994063543363,-36.0228998990979,5.28713246166602));
#6324=CARTESIAN_POINT('Ctrl Pts',(183.996782032333,-35.0023997001806,5.80856086039142));
#6325=CARTESIAN_POINT('',(183.402520572671,-35.,8.));
#6326=CARTESIAN_POINT('Ctrl Pts',(184.,-35.,5.80384757729336));
#6327=CARTESIAN_POINT('Ctrl Pts',(184.,-35.,6.26767582544512));
#6328=CARTESIAN_POINT('Ctrl Pts',(183.917463444079,-35.,6.72592757665807));
#6329=CARTESIAN_POINT('Ctrl Pts',(183.671800315476,-35.,7.45588656812286));
#6330=CARTESIAN_POINT('Ctrl Pts',(183.547885506158,-35.,7.73310336009194));
#6331=CARTESIAN_POINT('Ctrl Pts',(183.402520572671,-35.,8.00000000000001));
#6332=CARTESIAN_POINT('Ctrl Pts',(183.402520572671,-35.,8.));
#6333=CARTESIAN_POINT('Ctrl Pts',(183.212882493681,-35.3969969877486,8.));
#6334=CARTESIAN_POINT('Ctrl Pts',(182.944508993243,-35.8456903827968,8.00000000002023));
#6335=CARTESIAN_POINT('Ctrl Pts',(182.2724761698,-36.6776120047321,8.00000000002023));
#6336=CARTESIAN_POINT('Ctrl Pts',(181.971845249822,-36.9899807223263,8.));
#6337=CARTESIAN_POINT('Ctrl Pts',(181.667890676754,-37.2737119676906,8.));
#6338=CARTESIAN_POINT('Origin',(125.145502758917,-38.,0.));
#6339=CARTESIAN_POINT('',(125.145502758917,-35.,0.));
#6340=CARTESIAN_POINT('',(128.131421846764,-37.7096774193548,0.));
#6341=CARTESIAN_POINT('Origin',(124.,-38.,11.));
#6342=CARTESIAN_POINT('',(124.,-38.,8.));
#6343=CARTESIAN_POINT('',(180.898019313572,-35.,11.));
#6344=CARTESIAN_POINT('Origin',(180.898019313572,-38.,11.));
#6345=CARTESIAN_POINT('',(124.,-35.,11.));
#6346=CARTESIAN_POINT('Origin',(156.,-49.,8.));
#6347=CARTESIAN_POINT('',(183.368772894521,-35.,7.99999999999765));
#6348=CARTESIAN_POINT('',(0.,-35.,8.));
#6349=CARTESIAN_POINT('Ctrl Pts',(183.368772894519,-34.999999999999,8.));
#6350=CARTESIAN_POINT('Ctrl Pts',(183.128758753872,-35.4756885852746,8.));
#6351=CARTESIAN_POINT('Ctrl Pts',(182.837203794954,-35.9007967977573,8.));
#6352=CARTESIAN_POINT('Ctrl Pts',(182.271552980708,-36.6215015200439,8.));
#6353=CARTESIAN_POINT('Ctrl Pts',(181.974263989935,-36.9523893056604,8.));
#6354=CARTESIAN_POINT('Ctrl Pts',(181.667890676754,-37.2737119676906,8.));
#6355=CARTESIAN_POINT('Origin',(156.,-49.,8.));
#6356=CARTESIAN_POINT('',(152.,-50.,8.));
#6357=CARTESIAN_POINT('Origin',(156.,-50.,8.));
#6358=CARTESIAN_POINT('Ctrl Pts',(180.898019313572,-35.,11.));
#6359=CARTESIAN_POINT('Ctrl Pts',(180.908604851367,-35.,10.4283822830717));
#6360=CARTESIAN_POINT('Ctrl Pts',(180.933326641373,-35.3911165644152,9.09340871483843));
#6361=CARTESIAN_POINT('Ctrl Pts',(180.948707650874,-36.5547259255989,8.2628361256042));
#6362=CARTESIAN_POINT('Ctrl Pts',(180.952021751228,-37.2955742125391,8.08387512099361));
#6363=CARTESIAN_POINT('Ctrl Pts',(181.795578739617,-35.,11.0083107546761));
#6364=CARTESIAN_POINT('Ctrl Pts',(181.805136018515,-34.9983721392498,10.4383579957919));
#6365=CARTESIAN_POINT('Ctrl Pts',(181.827506908354,-35.3867659352872,9.10160449078975));
#6366=CARTESIAN_POINT('Ctrl Pts',(181.841477858758,-36.553089478282,8.26375258453703));
#6367=CARTESIAN_POINT('Ctrl Pts',(181.844474604683,-37.2936881269894,8.08433072812761));
#6368=CARTESIAN_POINT('Ctrl Pts',(183.349377359961,-34.246515734274,11.0226978122624));
#6369=CARTESIAN_POINT('Ctrl Pts',(183.357289972444,-34.2439912218348,10.307278215092));
#6370=CARTESIAN_POINT('Ctrl Pts',(183.375789434442,-34.7273862841715,8.63302779348577));
#6371=CARTESIAN_POINT('Ctrl Pts',(183.387325672956,-36.1854736296666,7.58707377292744));
#6372=CARTESIAN_POINT('Ctrl Pts',(183.38981428891,-37.115640232766,7.36157119560973));
#6373=CARTESIAN_POINT('Ctrl Pts',(183.897890720421,-32.6731984257692,11.0277766514379));
#6374=CARTESIAN_POINT('Ctrl Pts',(183.907279447281,-32.6724533308097,10.0123730883188));
#6375=CARTESIAN_POINT('Ctrl Pts',(183.92923478795,-33.3649359383542,7.64065313694788));
#6376=CARTESIAN_POINT('Ctrl Pts',(183.942925420429,-35.431438721091,6.16447437754468));
#6377=CARTESIAN_POINT('Ctrl Pts',(183.94586908761,-36.7483218632372,5.84612499706756));
#6378=CARTESIAN_POINT('Ctrl Pts',(183.897890720421,-32.,11.0277766514379));
#6379=CARTESIAN_POINT('Ctrl Pts',(183.908476258216,-32.,9.88454121758135));
#6380=CARTESIAN_POINT('Ctrl Pts',(183.933198048223,-32.7822331288305,7.21459408111476));
#6381=CARTESIAN_POINT('Ctrl Pts',(183.948579057724,-35.1094518511978,5.55344890264629));
#6382=CARTESIAN_POINT('Ctrl Pts',(183.951893158078,-36.5911484250781,5.19552689342511));
#6383=CARTESIAN_POINT('',(183.946003354294,-35.,5.83162422873126));
#6384=CARTESIAN_POINT('Ctrl Pts',(183.946003354294,-35.,5.83162422873127));
#6385=CARTESIAN_POINT('Ctrl Pts',(183.941587367144,-35.,6.30854973630342));
#6386=CARTESIAN_POINT('Ctrl Pts',(183.851877965836,-35.,6.83863274402651));
#6387=CARTESIAN_POINT('Ctrl Pts',(183.555890991522,-35.,7.61467203113213));
#6388=CARTESIAN_POINT('Ctrl Pts',(183.466406037598,-35.,7.81137594025207));
#6389=CARTESIAN_POINT('Ctrl Pts',(183.36877289452,-35.,7.99999999999715));
#6390=CARTESIAN_POINT('',(183.897890720421,-32.,11.0277766514379));
#6391=CARTESIAN_POINT('Origin',(183.897890720421,-38.,11.0277766514379));
#6392=CARTESIAN_POINT('Origin',(180.898019313572,-32.,11.));
#6393=CARTESIAN_POINT('Origin',(180.542507983541,-32.,49.3951347106504));
#6394=CARTESIAN_POINT('',(183.509279157931,-32.,52.9977281876795));
#6395=CARTESIAN_POINT('',(183.542379390391,-32.,49.4229113620883));
#6396=CARTESIAN_POINT('',(180.509407751081,-35.,52.9699515362416));
#6397=CARTESIAN_POINT('Origin',(180.509407751081,-32.,52.9699515362416));
#6398=CARTESIAN_POINT('',(180.542507983541,-35.,49.3951347106504));
#6399=CARTESIAN_POINT('Origin',(180.426077796767,22.9619250064101,61.969565756791));
#6400=CARTESIAN_POINT('',(183.472204154205,15.4757638065838,57.0018193155226));
#6401=CARTESIAN_POINT('',(183.509279157931,22.9619250064101,52.9977281876795));
#6402=CARTESIAN_POINT('Origin',(183.425949203617,22.9619250064101,61.9973424082289));
#6403=CARTESIAN_POINT('',(180.481631099643,22.9619250064101,55.9698229430914));
#6404=CARTESIAN_POINT('Origin',(180.509407751081,22.9619250064101,52.9699515362416));
#6405=CARTESIAN_POINT('',(180.456854989517,17.9668779442357,58.6456286919431));
#6406=CARTESIAN_POINT('Origin',(180.426077796767,22.9619250064101,61.969565756791));
#6407=CARTESIAN_POINT('Ctrl Pts',(180.456855041398,17.9668744188066,58.6456339902688));
#6408=CARTESIAN_POINT('Ctrl Pts',(180.464169860625,17.9668900378147,58.6456782485915));
#6409=CARTESIAN_POINT('Ctrl Pts',(180.471484765196,17.9668833841778,58.6457076852037));
#6410=CARTESIAN_POINT('Ctrl Pts',(180.875311709676,17.9652864766128,58.6465145041401));
#6411=CARTESIAN_POINT('Ctrl Pts',(181.267746602967,17.8982906281074,58.6037468164134));
#6412=CARTESIAN_POINT('Ctrl Pts',(181.993556182758,17.6431112722523,58.4372902978833));
#6413=CARTESIAN_POINT('Ctrl Pts',(182.320780158277,17.4591760990087,58.3164001965527));
#6414=CARTESIAN_POINT('Ctrl Pts',(182.872438697285,16.9974183098841,58.0116647840574));
#6415=CARTESIAN_POINT('Ctrl Pts',(183.091599797094,16.7240114613764,57.8307336627257));
#6416=CARTESIAN_POINT('Ctrl Pts',(183.391916275035,16.1229170096583,57.432110771519));
#6417=CARTESIAN_POINT('Ctrl Pts',(183.470200344055,15.8009765931121,57.218230310496));
#6418=CARTESIAN_POINT('Ctrl Pts',(183.472204154205,15.4757638065857,57.0018193155196));
#6419=CARTESIAN_POINT('Origin',(180.509407751081,17.5,52.9699515362416));
#6420=CARTESIAN_POINT('',(183.509279157931,32.,52.9977281876795));
#6421=CARTESIAN_POINT('',(180.481631099643,32.,55.9698229430914));
#6422=CARTESIAN_POINT('Origin',(180.509407751081,32.,52.9699515362416));
#6423=CARTESIAN_POINT('',(180.481631099643,17.5,55.9698229430914));
#6424=CARTESIAN_POINT('',(183.509279157931,17.5,52.9977281876795));
#6425=CARTESIAN_POINT('Ctrl Pts',(180.456854989517,17.9668779442357,58.6456286919431));
#6426=CARTESIAN_POINT('Ctrl Pts',(180.459728353753,17.5538362749007,59.2663537452259));
#6427=CARTESIAN_POINT('Ctrl Pts',(180.462961268117,17.2579323958192,59.9647514337378));
#6428=CARTESIAN_POINT('Ctrl Pts',(180.466333696842,17.0993058558373,60.6932880299539));
#6429=CARTESIAN_POINT('Ctrl Pts',(181.357372224078,17.9707236015583,58.6481877715177));
#6430=CARTESIAN_POINT('Ctrl Pts',(181.359700243583,17.5578731302105,59.2670196267812));
#6431=CARTESIAN_POINT('Ctrl Pts',(181.362326456225,17.2603980067746,59.9666372804095));
#6432=CARTESIAN_POINT('Ctrl Pts',(181.365055554869,17.1010357845145,60.6936647088526));
#6433=CARTESIAN_POINT('Ctrl Pts',(182.919937109513,17.3457188040812,58.23228045658));
#6434=CARTESIAN_POINT('Ctrl Pts',(182.920639258236,16.8800887242898,58.9295321606114));
#6435=CARTESIAN_POINT('Ctrl Pts',(182.921424127829,16.5458858994944,59.7141124557901));
#6436=CARTESIAN_POINT('Ctrl Pts',(182.922246255174,16.3658079346786,60.5335743996686));
#6437=CARTESIAN_POINT('Ctrl Pts',(183.47224362268,16.0316349538676,57.357827831654));
#6438=CARTESIAN_POINT('Ctrl Pts',(183.472236359704,15.4580713295682,58.2190205931141));
#6439=CARTESIAN_POINT('Ctrl Pts',(183.472252068947,15.0472514462844,59.1873279691006));
#6440=CARTESIAN_POINT('Ctrl Pts',(183.47224362268,14.826606833477,60.1984249895329));
#6441=CARTESIAN_POINT('Ctrl Pts',(183.47224362268,15.4693544131485,56.9836601598598));
#6442=CARTESIAN_POINT('Ctrl Pts',(183.47224362268,14.8497919091461,57.9147078318549));
#6443=CARTESIAN_POINT('Ctrl Pts',(183.47224362268,14.4059360905238,58.9622594629304));
#6444=CARTESIAN_POINT('Ctrl Pts',(183.47224362268,14.1679962805509,60.0550175178582));
#6445=CARTESIAN_POINT('',(180.466333696842,17.0993058558373,60.6932880299539));
#6446=CARTESIAN_POINT('Origin',(180.47224362268,22.9619250064101,61.9699932191321));
#6447=CARTESIAN_POINT('',(183.47224362268,14.1679962805509,60.0550175178582));
#6448=CARTESIAN_POINT('Origin',(180.47224362268,14.1679962805509,60.0550175178582));
#6449=CARTESIAN_POINT('',(183.47224362268,15.4601255574769,56.9975567301459));
#6450=CARTESIAN_POINT('Origin',(183.47224362268,22.9619250064101,61.9699932191321));
#6451=CARTESIAN_POINT('Ctrl Pts',(183.47224362268,15.460125717566,56.99755680507));
#6452=CARTESIAN_POINT('Ctrl Pts',(183.472243622256,15.4633487844854,56.9975568030941));
#6453=CARTESIAN_POINT('Ctrl Pts',(183.472239876315,15.4665745708394,56.9979465749962));
#6454=CARTESIAN_POINT('Ctrl Pts',(183.472230569335,15.4696494558241,56.9989155565643));
#6455=CARTESIAN_POINT('Ctrl Pts',(183.472223954011,15.4718350589064,56.9996043007328));
#6456=CARTESIAN_POINT('Ctrl Pts',(183.472214729775,15.4738784948292,57.0005647940433));
#6457=CARTESIAN_POINT('Ctrl Pts',(183.472202682799,15.4757640046251,57.0018195104561));
#6458=CARTESIAN_POINT('Ctrl Pts',(180.466333696842,17.0993058558373,60.6932880299539));
#6459=CARTESIAN_POINT('Ctrl Pts',(180.462827663279,16.6183159756739,62.9022409648325));
#6460=CARTESIAN_POINT('Ctrl Pts',(180.456117112077,14.7896202235287,67.1301787480821));
#6461=CARTESIAN_POINT('Ctrl Pts',(180.448438324107,9.85407602191408,71.9681476145139));
#6462=CARTESIAN_POINT('Ctrl Pts',(180.444297004961,3.45518438994196,74.57735797057));
#6463=CARTESIAN_POINT('Ctrl Pts',(180.444293007696,-3.45535478712963,74.5798764205847));
#6464=CARTESIAN_POINT('Ctrl Pts',(180.448441988675,-9.85267395691086,71.9658387779471));
#6465=CARTESIAN_POINT('Ctrl Pts',(180.456114870671,-14.7904585682235,67.1315909309643));
#6466=CARTESIAN_POINT('Ctrl Pts',(180.462827663279,-16.6183159756739,62.9022409648325));
#6467=CARTESIAN_POINT('Ctrl Pts',(180.466333696842,-17.0993058558373,60.6932880299539));
#6468=CARTESIAN_POINT('Ctrl Pts',(181.365055554869,17.1010357845145,60.6936647088526));
#6469=CARTESIAN_POINT('Ctrl Pts',(181.362218338067,16.6208107320077,62.9041865999037));
#6470=CARTESIAN_POINT('Ctrl Pts',(181.356777150885,14.7954594744657,67.1334068171006));
#6471=CARTESIAN_POINT('Ctrl Pts',(181.35054979597,9.85934073046915,71.9768075336286));
#6472=CARTESIAN_POINT('Ctrl Pts',(181.347185400725,3.45736101376534,74.5882859850751));
#6473=CARTESIAN_POINT('Ctrl Pts',(181.347183692439,-3.45785563298963,74.5914144228182));
#6474=CARTESIAN_POINT('Ctrl Pts',(181.350551527384,-9.85766669730974,71.9740201461265));
#6475=CARTESIAN_POINT('Ctrl Pts',(181.356775216638,-14.7971451523738,67.1347728987079));
#6476=CARTESIAN_POINT('Ctrl Pts',(181.362218338067,-16.6208107320077,62.9041865999037));
#6477=CARTESIAN_POINT('Ctrl Pts',(181.365055554869,-17.1010357845145,60.6936647088526));
#6478=CARTESIAN_POINT('Ctrl Pts',(182.922243752064,16.3658046786719,60.5335736906977));
#6479=CARTESIAN_POINT('Ctrl Pts',(182.921389054663,15.9071160601721,62.6479991065062));
#6480=CARTESIAN_POINT('Ctrl Pts',(182.919754407863,14.1594944560602,66.6966525066034));
#6481=CARTESIAN_POINT('Ctrl Pts',(182.917876131385,9.43644362697149,71.3316844154431));
#6482=CARTESIAN_POINT('Ctrl Pts',(182.916863279067,3.30915221594224,73.8324898890446));
#6483=CARTESIAN_POINT('Ctrl Pts',(182.916861444842,-3.30927917380312,73.8348409593045));
#6484=CARTESIAN_POINT('Ctrl Pts',(182.917877699306,-9.43511943897599,71.329525787935));
#6485=CARTESIAN_POINT('Ctrl Pts',(182.919753921885,-14.1602031813203,66.6980124501267));
#6486=CARTESIAN_POINT('Ctrl Pts',(182.921389054663,-15.9071160601721,62.6479991065062));
#6487=CARTESIAN_POINT('Ctrl Pts',(182.922243752064,-16.3658046786719,60.5335736906977));
#6488=CARTESIAN_POINT('Ctrl Pts',(183.47224362268,14.826606833477,60.1984249895329));
#6489=CARTESIAN_POINT('Ctrl Pts',(183.472252403561,14.4100919837911,62.1136233600875));
#6490=CARTESIAN_POINT('Ctrl Pts',(183.472249275606,12.824852883573,65.7803651712171));
#6491=CARTESIAN_POINT('Ctrl Pts',(183.472264206913,8.54564648381244,69.9763019277475));
#6492=CARTESIAN_POINT('Ctrl Pts',(183.472262740902,2.99650804402197,72.2398310923833));
#6493=CARTESIAN_POINT('Ctrl Pts',(183.472267398591,-2.99657429455144,72.2418653039269));
#6494=CARTESIAN_POINT('Ctrl Pts',(183.472260521092,-8.5444936796726,69.974419227184));
#6495=CARTESIAN_POINT('Ctrl Pts',(183.472248913357,-12.8253671346527,65.7816026321006));
#6496=CARTESIAN_POINT('Ctrl Pts',(183.472252403561,-14.4100919837911,62.1136233600875));
#6497=CARTESIAN_POINT('Ctrl Pts',(183.47224362268,-14.826606833477,60.1984249895329));
#6498=CARTESIAN_POINT('Ctrl Pts',(183.47224362268,14.1679962805509,60.0550175178582));
#6499=CARTESIAN_POINT('Ctrl Pts',(183.47224362268,13.7694618084156,61.885319704961));
#6500=CARTESIAN_POINT('Ctrl Pts',(183.47224362268,12.2542567566381,65.3885196371233));
#6501=CARTESIAN_POINT('Ctrl Pts',(183.47224362268,8.16480584672881,69.3971813236395));
#6502=CARTESIAN_POINT('Ctrl Pts',(183.47224362268,2.86286706595191,71.5591302478991));
#6503=CARTESIAN_POINT('Ctrl Pts',(183.47224362268,-2.86300825219312,71.5612169942924));
#6504=CARTESIAN_POINT('Ctrl Pts',(183.47224362268,-8.16364413572614,69.3952682595125));
#6505=CARTESIAN_POINT('Ctrl Pts',(183.47224362268,-12.2549513850995,65.3896897487074));
#6506=CARTESIAN_POINT('Ctrl Pts',(183.47224362268,-13.7694618084156,61.885319704961));
#6507=CARTESIAN_POINT('Ctrl Pts',(183.47224362268,-14.1679962805509,60.0550175178582));
#6508=CARTESIAN_POINT('',(180.466333696842,-17.0993058558373,60.6932880299539));
#6509=CARTESIAN_POINT('',(183.47224362268,-14.1679962805509,60.0550175178582));
#6510=CARTESIAN_POINT('Origin',(180.47224362268,-14.1679962805509,60.0550175178582));
#6511=CARTESIAN_POINT('Origin',(183.47224362268,0.,56.9697788880279));
#6512=CARTESIAN_POINT('Origin',(180.47224362268,0.,56.9697788880279));
#6513=CARTESIAN_POINT('Ctrl Pts',(180.466333696842,-17.0993058558373,60.6932880299539));
#6514=CARTESIAN_POINT('Ctrl Pts',(180.462961267011,-17.2579324478525,59.9647511947606));
#6515=CARTESIAN_POINT('Ctrl Pts',(180.459728351634,-17.5538364699809,59.2663532874908));
#6516=CARTESIAN_POINT('Ctrl Pts',(180.456854986689,-17.9668783506978,58.6456280811059));
#6517=CARTESIAN_POINT('Ctrl Pts',(181.365055554869,-17.1010357845145,60.6936647088526));
#6518=CARTESIAN_POINT('Ctrl Pts',(181.36232645533,-17.2603980590491,59.9666370419274));
#6519=CARTESIAN_POINT('Ctrl Pts',(181.359700241865,-17.5578733261006,59.2670191693394));
#6520=CARTESIAN_POINT('Ctrl Pts',(181.357372221785,-17.9707240084164,58.6481871616225));
#6521=CARTESIAN_POINT('Ctrl Pts',(182.922246255174,-16.3658079346786,60.5335743996685));
#6522=CARTESIAN_POINT('Ctrl Pts',(182.921424127559,-16.5458859585642,59.7141121869873));
#6523=CARTESIAN_POINT('Ctrl Pts',(182.92063925772,-16.8800889446273,58.9295316462732));
#6524=CARTESIAN_POINT('Ctrl Pts',(182.919937108823,-17.3457192622232,58.2322797705467));
#6525=CARTESIAN_POINT('Ctrl Pts',(183.47224362268,-14.826606833477,60.1984249895329));
#6526=CARTESIAN_POINT('Ctrl Pts',(183.472252068949,-15.047251518661,59.187327637437));
#6527=CARTESIAN_POINT('Ctrl Pts',(183.472236359702,-15.4580716004586,58.2190199582051));
#6528=CARTESIAN_POINT('Ctrl Pts',(183.47224362268,-16.0316355181454,57.3578269844147));
#6529=CARTESIAN_POINT('Ctrl Pts',(183.47224362268,-14.1679962805509,60.0550175178582));
#6530=CARTESIAN_POINT('Ctrl Pts',(183.47224362268,-14.4059361685737,58.96225910448));
#6531=CARTESIAN_POINT('Ctrl Pts',(183.47224362268,-14.8497922017664,57.9147071452817));
#6532=CARTESIAN_POINT('Ctrl Pts',(183.47224362268,-15.4693550228417,56.9836592436433));
#6533=CARTESIAN_POINT('',(183.47224362268,-15.4601255574769,56.9975567301459));
#6534=CARTESIAN_POINT('Origin',(183.47224362268,-22.9619250064101,61.9699932191321));
#6535=CARTESIAN_POINT('',(180.456855068753,-17.9668783510483,58.6456280813391));
#6536=CARTESIAN_POINT('Origin',(180.47224362268,-22.9619250064101,61.9699932191321));
#6537=CARTESIAN_POINT('',(183.472204154205,-15.4757638065838,57.0018193155226));
#6538=CARTESIAN_POINT('Ctrl Pts',(180.456855068753,-17.9668783510483,58.6456280813391));
#6539=CARTESIAN_POINT('Ctrl Pts',(180.464169869075,-17.9668926591679,58.6456743092186));
#6540=CARTESIAN_POINT('Ctrl Pts',(180.471484145303,-17.9668818389629,58.6457066556687));
#6541=CARTESIAN_POINT('Ctrl Pts',(180.478797763496,-17.9668498954977,58.6457192600464));
#6542=CARTESIAN_POINT('Ctrl Pts',(180.578070855833,-17.9664163034663,58.6458903484901));
#6543=CARTESIAN_POINT('Ctrl Pts',(180.676977830015,-17.9616130352007,58.6431515554912));
#6544=CARTESIAN_POINT('Ctrl Pts',(180.775213368172,-17.9526628202417,58.6376503408695));
#6545=CARTESIAN_POINT('Ctrl Pts',(180.87523702284,-17.943549690441,58.6320489912776));
#6546=CARTESIAN_POINT('Ctrl Pts',(180.974565314722,-17.9301370725114,58.6235836190736));
#6547=CARTESIAN_POINT('Ctrl Pts',(181.072876795846,-17.9126141567353,58.6123787823608));
#6548=CARTESIAN_POINT('Ctrl Pts',(181.172437383241,-17.8948686018158,58.6010315814843));
#6549=CARTESIAN_POINT('Ctrl Pts',(181.270955974619,-17.8729073888473,58.5868747071206));
#6550=CARTESIAN_POINT('Ctrl Pts',(181.368087710061,-17.8468838149634,58.5700080488639));
#6551=CARTESIAN_POINT('Ctrl Pts',(181.457022956091,-17.8230562478413,58.554564688412));
#6552=CARTESIAN_POINT('Ctrl Pts',(181.544795876943,-17.7958223204274,58.5368491259175));
#6553=CARTESIAN_POINT('Ctrl Pts',(181.631124895745,-17.7652713626968,58.5169185212022));
#6554=CARTESIAN_POINT('Ctrl Pts',(181.725234439151,-17.7319669568023,58.4951916426208));
#6555=CARTESIAN_POINT('Ctrl Pts',(181.817159917646,-17.6948871774175,58.4709408717903));
#6556=CARTESIAN_POINT('Ctrl Pts',(181.906575569164,-17.6542232102784,58.4442930581019));
#6557=CARTESIAN_POINT('Ctrl Pts',(181.99615909615,-17.6134828976408,58.4175952138639));
#6558=CARTESIAN_POINT('Ctrl Pts',(182.083224170943,-17.5691445827376,58.388491086226));
#6559=CARTESIAN_POINT('Ctrl Pts',(182.167424720833,-17.5213601095481,58.3570805184098));
#6560=CARTESIAN_POINT('Ctrl Pts',(182.25013097461,-17.4744236611358,58.3262273898202));
#6561=CARTESIAN_POINT('Ctrl Pts',(182.330074149522,-17.424161867348,58.2931486762449));
#6562=CARTESIAN_POINT('Ctrl Pts',(182.406897605853,-17.3706855018434,58.2579162124748));
#6563=CARTESIAN_POINT('Ctrl Pts',(182.472213528813,-17.3252194640436,58.2279612872582));
#6564=CARTESIAN_POINT('Ctrl Pts',(182.535274131469,-17.2774291143008,58.1964490729091));
#6565=CARTESIAN_POINT('Ctrl Pts',(182.595837938797,-17.2273663652658,58.1634125514998));
#6566=CARTESIAN_POINT('Ctrl Pts',(182.668050183894,-17.1676748818037,58.1240220064466));
#6567=CARTESIAN_POINT('Ctrl Pts',(182.736357538825,-17.1050472239898,58.0826594130257));
#6568=CARTESIAN_POINT('Ctrl Pts',(182.80042592618,-17.0396320551764,58.0394232766223));
#6569=CARTESIAN_POINT('Ctrl Pts',(182.804732571366,-17.035234880009,58.036516965001));
#6570=CARTESIAN_POINT('Ctrl Pts',(182.809020051043,-17.0308250966777,58.0336021791574));
#6571=CARTESIAN_POINT('Ctrl Pts',(182.813288258365,-17.026402744861,58.030678945324));
#6572=CARTESIAN_POINT('Ctrl Pts',(182.875945616796,-16.9614825425481,57.9877658213259));
#6573=CARTESIAN_POINT('Ctrl Pts',(182.934453087186,-16.8938562039598,57.9430337528228));
#6574=CARTESIAN_POINT('Ctrl Pts',(182.988728507397,-16.8238623650039,57.896707024575));
#6575=CARTESIAN_POINT('Ctrl Pts',(183.04366780639,-16.7530123848283,57.8498136432871));
#6576=CARTESIAN_POINT('Ctrl Pts',(183.094271276253,-16.6797359604965,57.8012858973768));
#6577=CARTESIAN_POINT('Ctrl Pts',(183.14040883038,-16.6043605384826,57.7513404279431));
#6578=CARTESIAN_POINT('Ctrl Pts',(183.176387827286,-16.5455812614554,57.7123919417435));
#6579=CARTESIAN_POINT('Ctrl Pts',(183.209650168388,-16.4855249573283,57.6725809164522));
#6580=CARTESIAN_POINT('Ctrl Pts',(183.240113291573,-16.4243411280662,57.6320062199135));
#6581=CARTESIAN_POINT('Ctrl Pts',(183.279095707768,-16.3460466773555,57.5800844357336));
#6582=CARTESIAN_POINT('Ctrl Pts',(183.313304429564,-16.2662909288594,57.5271679917355));
#6583=CARTESIAN_POINT('Ctrl Pts',(183.342661685082,-16.1854199607586,57.4734863710623));
#6584=CARTESIAN_POINT('Ctrl Pts',(183.372088662144,-16.1043569294474,57.4196772600839));
#6585=CARTESIAN_POINT('Ctrl Pts',(183.396641398369,-16.0221726384945,57.3650988382935));
#6586=CARTESIAN_POINT('Ctrl Pts',(183.416194188832,-15.9391967318707,57.3099699346756));
#6587=CARTESIAN_POINT('Ctrl Pts',(183.435389595124,-15.857737451516,57.2558486722733));
#6588=CARTESIAN_POINT('Ctrl Pts',(183.449766291803,-15.7755145143301,57.2011963891436));
#6589=CARTESIAN_POINT('Ctrl Pts',(183.459156841502,-15.6928324349362,57.1462155529733));
#6590=CARTESIAN_POINT('Ctrl Pts',(183.467342656943,-15.6207578212171,57.098288329106));
#6591=CARTESIAN_POINT('Ctrl Pts',(183.471739016432,-15.5483339332306,57.0501111947275));
#6592=CARTESIAN_POINT('Ctrl Pts',(183.472202682799,-15.4757640046365,57.0018195104682));
#6593=CARTESIAN_POINT('Ctrl Pts',(183.472202682799,-15.4757640046365,57.0018195104682));
#6594=CARTESIAN_POINT('Ctrl Pts',(183.472211127192,-15.4744423453996,57.000940011793));
#6595=CARTESIAN_POINT('Ctrl Pts',(183.472218262832,-15.4730308628213,57.0001969339396));
#6596=CARTESIAN_POINT('Ctrl Pts',(183.472224092048,-15.4715297601456,56.9995899676826));
#6597=CARTESIAN_POINT('Ctrl Pts',(183.472238137763,-15.4679127966574,56.9981274596038));
#6598=CARTESIAN_POINT('Ctrl Pts',(183.472243622167,-15.4640255998031,56.9975568026889));
#6599=CARTESIAN_POINT('Ctrl Pts',(183.47224362268,-15.4601257175872,56.9975568050799));
#6600=CARTESIAN_POINT('Origin',(180.426077796767,-22.9619250064101,61.969565756791));
#6601=CARTESIAN_POINT('',(180.481631099643,-22.9619250064101,55.9698229430914));
#6602=CARTESIAN_POINT('Origin',(180.426077796767,-22.9619250064101,61.969565756791));
#6603=CARTESIAN_POINT('',(183.509279157931,-22.9619250064101,52.9977281876795));
#6604=CARTESIAN_POINT('Origin',(180.509407751081,-22.9619250064101,52.9699515362416));
#6605=CARTESIAN_POINT('Origin',(183.425949203617,-22.9619250064101,61.9973424082289));
#6606=CARTESIAN_POINT('Origin',(180.509407751081,-11.480962503205,52.9699515362416));
#6607=CARTESIAN_POINT('',(180.481631099643,-32.,55.9698229430914));
#6608=CARTESIAN_POINT('Origin',(180.509407751081,-32.,52.9699515362416));
#6609=CARTESIAN_POINT('',(183.509279157931,-11.480962503205,52.9977281876795));
#6610=CARTESIAN_POINT('',(180.481631099643,-11.480962503205,55.9698229430914));
#6611=CARTESIAN_POINT('Origin',(180.542507983541,32.,49.3951347106504));
#6612=CARTESIAN_POINT('Origin',(180.509407751081,32.,52.9699515362416));
#6613=CARTESIAN_POINT('',(183.542379390391,32.,49.4229113620883));
#6614=CARTESIAN_POINT('Origin',(180.509407751081,32.,52.9699515362416));
#6615=CARTESIAN_POINT('Origin',(180.509407751081,32.,52.9699515362416));
#6616=CARTESIAN_POINT('Origin',(180.509407751081,-32.,52.9699515362416));
#6617=CARTESIAN_POINT('Origin',(180.509407751081,-32.,52.9699515362416));
#6618=CARTESIAN_POINT('Origin',(156.,-35.,0.));
#6619=CARTESIAN_POINT('',(184.,-35.,0.));
#6620=CARTESIAN_POINT('Origin',(92.,-35.,41.));
#6621=CARTESIAN_POINT('',(60.,-35.,11.));
#6622=CARTESIAN_POINT('',(158.47224362268,-35.,52.7659032476128));
#6623=CARTESIAN_POINT('',(137.703021578879,-35.,52.5735951906642));
#6624=CARTESIAN_POINT('',(158.47224362268,-35.,37.));
#6625=CARTESIAN_POINT('',(158.47224362268,-35.,74.9975567301459));
#6626=CARTESIAN_POINT('',(158.47224362268,-35.,37.));
#6627=CARTESIAN_POINT('',(31.47224362268,-35.,82.));
#6628=CARTESIAN_POINT('Origin',(137.703021578879,-32.,52.5735951906642));
#6629=CARTESIAN_POINT('',(158.47224362268,-32.,55.7660318462753));
#6630=CARTESIAN_POINT('',(137.675244927441,-32.,55.573466597514));
#6631=CARTESIAN_POINT('Origin',(158.47224362268,-32.,52.7659032476128));
#6632=CARTESIAN_POINT('Origin',(183.481502506493,-22.9619250064101,55.9975995945293));
#6633=CARTESIAN_POINT('',(158.47224362268,-22.9619250064101,55.7660318462753));
#6634=CARTESIAN_POINT('',(183.481502506493,-22.9619250064101,55.9975995945293));
#6635=CARTESIAN_POINT('',(158.47224362268,-11.480962503205,55.7660318462753));
#6636=CARTESIAN_POINT('Origin',(183.425949203617,-22.9619250064101,61.9973424082289));
#6637=CARTESIAN_POINT('',(158.47224362268,-17.0993058558373,60.4896385760844));
#6638=CARTESIAN_POINT('',(183.437769055293,-17.0993058558373,60.7208013840375));
#6639=CARTESIAN_POINT('Origin',(158.47224362268,-22.9619250064101,61.7662890436003));
#6640=CARTESIAN_POINT('Origin',(183.47224362268,0.,56.9975567301459));
#6641=CARTESIAN_POINT('',(158.47224362268,17.0993058558373,60.4896385760844));
#6642=CARTESIAN_POINT('',(183.437769055293,17.0993058558373,60.7208013840375));
#6643=CARTESIAN_POINT('Origin',(158.47224362268,0.,56.7660747124961));
#6644=CARTESIAN_POINT('Origin',(183.425949203617,22.9619250064101,61.9973424082289));
#6645=CARTESIAN_POINT('',(158.47224362268,22.9619250064101,55.7660318462753));
#6646=CARTESIAN_POINT('',(183.481502506493,22.9619250064101,55.9975995945293));
#6647=CARTESIAN_POINT('Origin',(158.47224362268,22.9619250064101,61.7662890436003));
#6648=CARTESIAN_POINT('Origin',(183.481502506493,35.,55.9975995945293));
#6649=CARTESIAN_POINT('',(158.47224362268,32.,55.7660318462753));
#6650=CARTESIAN_POINT('',(137.675244927441,32.,55.573466597514));
#6651=CARTESIAN_POINT('',(158.47224362268,17.5,55.7660318462753));
#6652=CARTESIAN_POINT('Origin',(137.703021578879,32.,52.5735951906642));
#6653=CARTESIAN_POINT('Origin',(158.47224362268,32.,52.7659032476128));
#6654=CARTESIAN_POINT('Origin',(158.47224362268,0.,37.));
#6655=CARTESIAN_POINT('',(158.47224362268,0.,37.));
#6656=CARTESIAN_POINT('',(158.47224362268,-9.5,56.9975567301459));
#6657=CARTESIAN_POINT('Origin',(158.47224362268,0.,56.9975567301459));
#6658=CARTESIAN_POINT('Origin',(183.47224362268,0.,56.9975567301459));
#6659=CARTESIAN_POINT('',(183.47224362268,9.5,56.9975567301459));
#6660=CARTESIAN_POINT('',(183.47224362268,-9.5,56.9975567301459));
#6661=CARTESIAN_POINT('Origin',(183.47224362268,0.,56.9975567301459));
#6662=CARTESIAN_POINT('Origin',(183.47224362268,0.,56.9975567301459));
#6663=CARTESIAN_POINT('',(183.47224362268,-9.5,56.9975567301459));
#6664=CARTESIAN_POINT('Origin',(183.47224362268,0.,74.9975567301459));
#6665=CARTESIAN_POINT('',(183.47224362268,0.,56.9975567301459));
#6666=CARTESIAN_POINT('',(183.47224362268,0.,56.9975567301459));
#6667=CARTESIAN_POINT('Origin',(125.145502758917,38.,0.));
#6668=CARTESIAN_POINT('Origin',(125.145502758917,38.,0.));
#6669=CARTESIAN_POINT('Origin',(124.,38.,11.));
#6670=CARTESIAN_POINT('',(124.,38.,8.));
#6671=CARTESIAN_POINT('Origin',(156.,49.,8.));
#6672=CARTESIAN_POINT('',(152.,50.,8.));
#6673=CARTESIAN_POINT('Origin',(156.,50.,8.));
#6674=CARTESIAN_POINT('Origin',(60.,-38.,11.));
#6675=CARTESIAN_POINT('Origin',(28.,50.,0.));
#6676=CARTESIAN_POINT('',(24.,50.,0.));
#6677=CARTESIAN_POINT('',(24.,50.,0.));
#6678=CARTESIAN_POINT('Origin',(28.,50.,0.));
#6679=CARTESIAN_POINT('Origin',(28.,35.,0.));
#6680=CARTESIAN_POINT('Origin',(28.,35.,0.));
#6681=CARTESIAN_POINT('Origin',(28.,-50.,0.));
#6682=CARTESIAN_POINT('',(24.,-50.,0.));
#6683=CARTESIAN_POINT('Origin',(156.,50.,0.));
#6684=CARTESIAN_POINT('',(152.,50.,0.));
#6685=CARTESIAN_POINT('',(152.,50.,0.));
#6686=CARTESIAN_POINT('Origin',(156.,50.,0.));
#6687=CARTESIAN_POINT('Origin',(156.,-50.,0.));
#6688=CARTESIAN_POINT('',(152.,-50.,0.));
#6689=CARTESIAN_POINT('Origin',(184.,-35.,0.));
#6690=CARTESIAN_POINT('',(184.,-35.,0.));
#6691=CARTESIAN_POINT('Origin',(10.8741674113267,19.,62.));
#6692=CARTESIAN_POINT('',(13.47224362268,16.,62.));
#6693=CARTESIAN_POINT('Origin',(13.47224362268,19.,62.));
#6694=CARTESIAN_POINT('',(8.27609119997336,19.,62.));
#6695=CARTESIAN_POINT('',(10.8741674113267,17.5,62.));
#6696=CARTESIAN_POINT('Origin',(22.47224362268,19.,62.));
#6697=CARTESIAN_POINT('',(22.47224362268,16.,62.));
#6698=CARTESIAN_POINT('Origin',(10.8741674113267,-19.,62.));
#6699=CARTESIAN_POINT('',(13.47224362268,-22.,62.));
#6700=CARTESIAN_POINT('Origin',(13.47224362268,-19.,62.));
#6701=CARTESIAN_POINT('',(8.27609119997336,-19.,62.));
#6702=CARTESIAN_POINT('',(10.8741674113267,-20.5,62.));
#6703=CARTESIAN_POINT('Origin',(22.47224362268,-19.,62.));
#6704=CARTESIAN_POINT('',(22.47224362268,-22.,62.));
#6705=CARTESIAN_POINT('Origin',(31.47224362268,0.,37.));
#6706=CARTESIAN_POINT('Origin',(16.97224362268,0.,82.));
#6707=CARTESIAN_POINT('',(16.97224362268,0.,82.));
#6708=CARTESIAN_POINT('Origin',(35.,0.,52.));
#6709=CARTESIAN_POINT('Origin',(184.,0.,0.));
#6710=CARTESIAN_POINT('',(184.,0.,0.));
#6711=CARTESIAN_POINT('Origin',(183.47224362268,0.,56.9975567301459));
#8425=UNCERTAINTY_MEASURE_WITH_UNIT(LENGTH_MEASURE(0.01),#8446,
'DISTANCE_ACCURACY_VALUE',
'Maximum model space distance between geometric entities at asserted c
onnectivities');
#8434=UNCERTAINTY_MEASURE_WITH_UNIT(LENGTH_MEASURE(0.01),#8446,
'DISTANCE_ACCURACY_VALUE',
'Maximum model space distance between geometric entities at asserted c
onnectivities');
#8436=(
GEOMETRIC_REPRESENTATION_CONTEXT(3)
GLOBAL_UNCERTAINTY_ASSIGNED_CONTEXT((#8425))
GLOBAL_UNIT_ASSIGNED_CONTEXT((#8446,#8448,#8449))
REPRESENTATION_CONTEXT('','3D')
);
#8445=(
GEOMETRIC_REPRESENTATION_CONTEXT(3)
GLOBAL_UNCERTAINTY_ASSIGNED_CONTEXT((#8434))
GLOBAL_UNIT_ASSIGNED_CONTEXT((#8446,#8448,#8449))
REPRESENTATION_CONTEXT('','3D')
);
#8446=(
LENGTH_UNIT()
NAMED_UNIT(*)
SI_UNIT(.MILLI.,.METRE.)
);
#8448=(
NAMED_UNIT(*)
PLANE_ANGLE_UNIT()
SI_UNIT($,.RADIAN.)
);
#8449=(
NAMED_UNIT(*)
SI_UNIT($,.STERADIAN.)
SOLID_ANGLE_UNIT()
);
#8451=SHAPE_DEFINITION_REPRESENTATION(#8461,#8484);
#8461=PRODUCT_DEFINITION_SHAPE('',$,#8495);
#8484=SHAPE_REPRESENTATION('',(#4112),#8436);
#8493=PRODUCT_DEFINITION_CONTEXT('part definition',#8525,'design');
#8495=PRODUCT_DEFINITION('2026-10-05-16-34-41-040','Configuration 1',#8505,
#8493);
#8505=PRODUCT_DEFINITION_FORMATION('',$,#8528);
#8525=APPLICATION_CONTEXT(
'Core Data for Automotive Mechanical Design Process');
#8526=PRODUCT_CONTEXT('part definition',#8525,'mechanical');
#8528=PRODUCT('2026-10-05-16-34-41-040','Configuration 1',$,(#8526));
#8537=PRESENTATION_STYLE_ASSIGNMENT((#8538));
#8538=SURFACE_STYLE_USAGE(.BOTH.,#8539);
#8539=SURFACE_SIDE_STYLE('',(#8540));
#8540=SURFACE_STYLE_FILL_AREA(#8541);
#8541=FILL_AREA_STYLE('Steel - Satin',(#8542));
#8542=FILL_AREA_STYLE_COLOUR('Steel - Satin',#8543);
#8543=COLOUR_RGB('Steel - Satin', 0.09019608, 0.27058824, 0.51372549);
ENDSEC;
END-ISO-10303-21;
